ISO-10303-21;
HEADER;
FILE_DESCRIPTION (('STEP AP214'),
    '1' );
FILE_NAME ('Snap Open Cable Crossbars 13.step',
    '2026-10-08T22:59:04',
    ( '' ),
    ( '' ),
    'SwSTEP 2.0',
    'SolidWorks 2020',
    '' );
FILE_SCHEMA (( 'AUTOMOTIVE_DESIGN' ));
ENDSEC;

DATA;
#240=LINE ( 'NONE', #240155, #250850 ) ;
#314=AXIS2_PLACEMENT_3D ( 'NONE', #40816, #102008, #159455 ) ;
#662=CARTESIAN_POINT ( 'NONE',  ( -18.40000000000000213, 64.25000000001199396, -112.2731074845243739 ) ) ;
#875=CARTESIAN_POINT ( 'NONE',  ( -16.88219499860498374, 66.04979357458446998, -123.8737977944170581 ) ) ;
#912=EDGE_CURVE ( 'NONE', #150586, #28814, #180624, .T. ) ;
#937=B_SPLINE_CURVE_WITH_KNOTS ( 'NONE', 3,
 ( #16436, #256229, #95929, #254954, #76368, #56786, #112952, #37281, #77643, #73851 ),
 .UNSPECIFIED., .F., .F.,
 ( 4, 2, 2, 2, 4 ),
 ( 5.329075035707888194E-16, 9.930191194499807640E-05, 0.0001986038238894632403, 0.0003972076477784337650, 0.0007944152955563318257 ),
 .UNSPECIFIED. ) ;
#1233=ADVANCED_FACE ( 'NONE', ( #109429 ), #132875, .F. ) ;
#1285=CARTESIAN_POINT ( 'NONE',  ( -16.81453563122427752, 66.06089979457505024, -115.7348488238790338 ) ) ;
#1288=EDGE_LOOP ( 'NONE', ( #222345, #60721, #222413, #103347 ) ) ;
#1334=CARTESIAN_POINT ( 'NONE',  ( -18.40000000000000213, 64.52683809664951298, -115.5731074845243853 ) ) ;
#1341=DIRECTION ( 'NONE',  ( -0.000000000000000000, -6.982962677686266711E-15, 1.000000000000000000 ) ) ;
#1471=ORIENTED_EDGE ( 'NONE', *, *, #52588, .F. ) ;
#1528=AXIS2_PLACEMENT_3D ( 'NONE', #7515, #141884, #87026 ) ;
#1681=ORIENTED_EDGE ( 'NONE', *, *, #32691, .T. ) ;
#2046=CARTESIAN_POINT ( 'NONE',  ( -16.91256925476571382, 66.01426884188386168, -123.9907499735296454 ) ) ;
#2072=CARTESIAN_POINT ( 'NONE',  ( -23.25000000000000355, 65.95000000001201101, -115.7731074845243597 ) ) ;
#2425=AXIS2_PLACEMENT_3D ( 'NONE', #153513, #135160, #16531 ) ;
#2664=VECTOR ( 'NONE', #201479, 1000.000000000000000 ) ;
#2718=ADVANCED_FACE ( 'NONE', ( #169225 ), #124935, .F. ) ;
#3055=CARTESIAN_POINT ( 'NONE',  ( -16.87683809663752399, 66.15000000001207070, -123.8731074845243683 ) ) ;
#3083=SHAPE_REPRESENTATION_RELATIONSHIP ( 'NONE' , 'NONE' ,  #73451, #119926 ) ;
#3092=AXIS2_PLACEMENT_3D ( 'NONE', #188305, #125756, #9671 ) ;
#3311=CARTESIAN_POINT ( 'NONE',  ( -16.86578989773641979, 66.01519019875325966, -123.9877723711466047 ) ) ;
#3328=LINE ( 'NONE', #37363, #107087 ) ;
#3365=CARTESIAN_POINT ( 'NONE',  ( -17.29158576265543346, 65.63525233399415981, -125.1058657293165339 ) ) ;
#3458=DIRECTION ( 'NONE',  ( 1.000000000000000000, 0.000000000000000000, 0.000000000000000000 ) ) ;
#3538=PRODUCT_DEFINITION_CONTEXT ( 'detailed design', #205831, 'design' ) ;
#3779=( BOUNDED_CURVE ( )  B_SPLINE_CURVE ( 3, ( #133703, #148137, #228966, #213227 ),
 .UNSPECIFIED., .F., .T. ) 
 B_SPLINE_CURVE_WITH_KNOTS ( ( 4, 4 ),
 ( 0.5235987755982449698, 1.570796326794896558 ),
 .UNSPECIFIED. ) 
 CURVE ( )  GEOMETRIC_REPRESENTATION_ITEM ( )  RATIONAL_B_SPLINE_CURVE ( ( 1.000000000000000000, 0.9106836025229499976, 0.9106836025229499976, 1.000000000000000000 ) ) 
 REPRESENTATION_ITEM ( '' )  );
#3836=ADVANCED_FACE ( 'NONE', ( #227925 ), #196486, .F. ) ;
#3872=VERTEX_POINT ( 'NONE', #191398 ) ;
#3945=ORIENTED_EDGE ( 'NONE', *, *, #118195, .F. ) ;
#4083=CARTESIAN_POINT ( 'NONE',  ( -16.94445028196807002, 66.00793639031427062, -115.6304376629428106 ) ) ;
#4141=DIRECTION ( 'NONE',  ( -1.000000000000000000, -0.000000000000000000, -0.000000000000000000 ) ) ;
#4154=VERTEX_POINT ( 'NONE', #90655 ) ;
#4175=LINE ( 'NONE', #60294, #24131 ) ;
#4379=FILL_AREA_STYLE ('',( #140027 ) ) ;
#4407=CARTESIAN_POINT ( 'NONE',  ( -16.93415306273742260, 66.00437773999949798, -115.6130505421639612 ) ) ;
#4445=CARTESIAN_POINT ( 'NONE',  ( -16.93710578446422943, 66.05000000001201954, -115.9419114683237098 ) ) ;
#4620=EDGE_CURVE ( 'NONE', #124526, #191326, #56349, .T. ) ;
#4678=EDGE_CURVE ( 'NONE', #12698, #64183, #240, .T. ) ;
#4736=PLANE ( 'NONE',  #31685 ) ;
#4924=VECTOR ( 'NONE', #143583, 1000.000000000000000 ) ;
#5370=DIRECTION ( 'NONE',  ( 1.000000000000000000, 0.000000000000000000, 0.000000000000000000 ) ) ;
#5561=ORIENTED_EDGE ( 'NONE', *, *, #13863, .T. ) ;
#5646=VERTEX_POINT ( 'NONE', #244333 ) ;
#5672=CARTESIAN_POINT ( 'NONE',  ( -16.93344882324368683, 66.00341123272413313, -115.6100817897194446 ) ) ;
#5713=CARTESIAN_POINT ( 'NONE',  ( -16.89935556175729303, 66.05000000001200533, -116.1627838474090879 ) ) ;
#5716=CARTESIAN_POINT ( 'NONE',  ( -21.64999999999999858, 66.65000000001209912, -127.2731074845243597 ) ) ;
#5820=EDGE_CURVE ( 'NONE', #30385, #143067, #206060, .T. ) ;
#5969=LINE ( 'NONE', #183356, #211709 ) ;
#5988=DIRECTION ( 'NONE',  ( 0.000000000000000000, -6.982962677686266711E-15, 1.000000000000000000 ) ) ;
#6008=EDGE_CURVE ( 'NONE', #78597, #149927, #157685, .T. ) ;
#6282=EDGE_CURVE ( 'NONE', #120700, #19871, #90266, .T. ) ;
#6350=EDGE_CURVE ( 'NONE', #239536, #56104, #164638, .T. ) ;
#6360=ORIENTED_EDGE ( 'NONE', *, *, #128761, .F. ) ;
#6734=CIRCLE ( 'NONE', #69296, 0.09999999999999516220 ) ;
#6735=CARTESIAN_POINT ( 'NONE',  ( -17.01473183483380680, 66.05000000001201954, -115.7731074845243739 ) ) ;
#6918=DIRECTION ( 'NONE',  ( -0.000000000000000000, -6.982962677686266711E-15, 1.000000000000000000 ) ) ;
#7011=EDGE_CURVE ( 'NONE', #212706, #184009, #23575, .T. ) ;
#7105=ORIENTED_EDGE ( 'NONE', *, *, #92846, .T. ) ;
#7173=DIRECTION ( 'NONE',  ( -1.000000000000000000, 0.000000000000000000, 0.000000000000000000 ) ) ;
#7208=VERTEX_POINT ( 'NONE', #173772 ) ;
#7306=PLANE ( 'NONE',  #207492 ) ;
#7394=CYLINDRICAL_SURFACE ( 'NONE', #103913, 0.9000000000000014655 ) ;
#7515=CARTESIAN_POINT ( 'NONE',  ( -14.00000000000000178, 66.15000000001204228, -119.7731074845243739 ) ) ;
#7935=VERTEX_POINT ( 'NONE', #248799 ) ;
#8001=CARTESIAN_POINT ( 'NONE',  ( -18.44085059012131822, 64.48598750652818978, -112.2828021654028419 ) ) ;
#8094=DIRECTION ( 'NONE',  ( -1.000000000000000000, 0.000000000000000000, -0.000000000000000000 ) ) ;
#8321=FACE_OUTER_BOUND ( 'NONE', #190599, .T. ) ;
#8330=CARTESIAN_POINT ( 'NONE',  ( -16.83233564386400971, 66.06977820342747520, -115.7985868210489997 ) ) ;
#8339=CARTESIAN_POINT ( 'NONE',  ( -20.65000000000000568, 68.75000000001207923, -123.8731074845243540 ) ) ;
#8364=CYLINDRICAL_SURFACE ( 'NONE', #200842, 0.09999999999999939493 ) ;
#8372=CARTESIAN_POINT ( 'NONE',  ( -14.77738660682464200, 66.56344716000762674, -121.3451520117640712 ) ) ;
#8474=ORIENTED_EDGE ( 'NONE', *, *, #95101, .T. ) ;
#8672=ORIENTED_EDGE ( 'NONE', *, *, #164104, .T. ) ;
#8756=CARTESIAN_POINT ( 'NONE',  ( -16.89797118371608775, 66.02361927736821201, -123.9604008520823157 ) ) ;
#8919=ORIENTED_EDGE ( 'NONE', *, *, #49941, .F. ) ;
#9100=ORIENTED_EDGE ( 'NONE', *, *, #202724, .T. ) ;
#9160=CARTESIAN_POINT ( 'NONE',  ( -18.35235881385853318, 64.52658099229918776, -127.2731074845243882 ) ) ;
#9221=CARTESIAN_POINT ( 'NONE',  ( 20.27550659511088682, 66.78395627750323627, -127.2731074845243597 ) ) ;
#9503=EDGE_CURVE ( 'NONE', #39978, #208088, #212274, .T. ) ;
#9576=CARTESIAN_POINT ( 'NONE',  ( -16.85697194749132422, 66.09145628588846932, -123.5881032169100564 ) ) ;
#9588=ORIENTED_EDGE ( 'NONE', *, *, #158958, .F. ) ;
#9591=ADVANCED_FACE ( 'NONE', ( #16352 ), #31524, .T. ) ;
#9671=DIRECTION ( 'NONE',  ( 0.000000000000000000, 0.000000000000000000, 1.000000000000000000 ) ) ;
#9830=VERTEX_POINT ( 'NONE', #8339 ) ;
#9867=CARTESIAN_POINT ( 'NONE',  ( -20.65000000000000568, 70.35000000001207354, -123.8731074845243398 ) ) ;
#9971=FACE_OUTER_BOUND ( 'NONE', #31274, .T. ) ;
#10032=CARTESIAN_POINT ( 'NONE',  ( -16.92570016628985385, 66.04121104227219519, -123.9024568144853760 ) ) ;
#10075=EDGE_CURVE ( 'NONE', #4154, #31295, #181444, .T. ) ;
#10309=CARTESIAN_POINT ( 'NONE',  ( -16.77683809663752257, 66.05416425680785153, -115.6870565036285683 ) ) ;
#10416=VERTEX_POINT ( 'NONE', #153909 ) ;
#10655=LINE ( 'NONE', #90162, #187155 ) ;
#10880=CARTESIAN_POINT ( 'NONE',  ( -16.85722902420150149, 66.05000000001206217, -123.7575600107535934 ) ) ;
#10952=ORIENTED_EDGE ( 'NONE', *, *, #40129, .F. ) ;
#11320=( BOUNDED_CURVE ( )  B_SPLINE_CURVE ( 3, ( #54864, #250506, #148868, #151437 ),
 .UNSPECIFIED., .F., .F. ) 
 B_SPLINE_CURVE_WITH_KNOTS ( ( 4, 4 ),
 ( 5.733388419619901200, 5.983100554402347449 ),
 .UNSPECIFIED. ) 
 CURVE ( )  GEOMETRIC_REPRESENTATION_ITEM ( )  RATIONAL_B_SPLINE_CURVE ( ( 1.000000000000000000, 0.9948104011409417691, 0.9948104011409417691, 1.000000000000000000 ) ) 
 REPRESENTATION_ITEM ( '' )  );
#11466=FACE_OUTER_BOUND ( 'NONE', #221769, .T. ) ;
#11866=CARTESIAN_POINT ( 'NONE',  ( -17.80356949363585528, 65.12326860301367049, -113.3100344602850953 ) ) ;
#12012=VERTEX_POINT ( 'NONE', #219971 ) ;
#12119=ORIENTED_EDGE ( 'NONE', *, *, #192141, .F. ) ;
#12505=CARTESIAN_POINT ( 'NONE',  ( -21.64999999999999858, 65.95000000001201101, -115.7731074845243597 ) ) ;
#12698=VERTEX_POINT ( 'NONE', #113841 ) ;
#12699=ORIENTED_EDGE ( 'NONE', *, *, #234019, .F. ) ;
#12720=ADVANCED_FACE ( 'NONE', ( #70898 ), #35628, .F. ) ;
#12809=DIRECTION ( 'NONE',  ( -1.646408749285562691E-14, -1.000000000000000000, -6.982962677686266711E-15 ) ) ;
#12850=DIRECTION ( 'NONE',  ( -1.652117596168391700E-15, 1.000000000000000000, 6.982962677686266711E-15 ) ) ;
#13014=VECTOR ( 'NONE', #78477, 1000.000000000000000 ) ;
#13037=CARTESIAN_POINT ( 'NONE',  ( -16.78569801330232281, 66.05206626689856364, -123.8661945791768630 ) ) ;
#13365=DIRECTION ( 'NONE',  ( 0.000000000000000000, 1.000000000000000000, 6.982962677686266711E-15 ) ) ;
#13443=CARTESIAN_POINT ( 'NONE',  ( -18.34374000495060386, 64.52683809664961245, -127.2731074845243882 ) ) ;
#13471=DIRECTION ( 'NONE',  ( 0.000000000000000000, -6.982962677686266711E-15, 1.000000000000000000 ) ) ;
#13482=CARTESIAN_POINT ( 'NONE',  ( -16.93935632781549572, 66.01526950028690521, -115.6334467358140614 ) ) ;
#13507=EDGE_CURVE ( 'NONE', #109222, #175428, #60616, .T. ) ;
#13592=LINE ( 'NONE', #172705, #216026 ) ;
#13858=VERTEX_POINT ( 'NONE', #97804 ) ;
#13863=EDGE_CURVE ( 'NONE', #212706, #30748, #118076, .T. ) ;
#14020=CARTESIAN_POINT ( 'NONE',  ( 13.54577453029515688, 66.54939790392350574, -118.0792115214276947 ) ) ;
#14074=CARTESIAN_POINT ( 'NONE',  ( -16.93658211146646408, 66.00589133767087446, -123.9274025544800537 ) ) ;
#14146=( GEOMETRIC_REPRESENTATION_CONTEXT ( 3 ) GLOBAL_UNCERTAINTY_ASSIGNED_CONTEXT ( ( #255317 ) ) GLOBAL_UNIT_ASSIGNED_CONTEXT ( ( #124534, #146630, #168834 ) ) REPRESENTATION_CONTEXT ( 'NONE', 'WORKASPACE' ) );
#14308=VERTEX_POINT ( 'NONE', #157547 ) ;
#14584=ORIENTED_EDGE ( 'NONE', *, *, #232883, .T. ) ;
#14773=EDGE_CURVE ( 'NONE', #186539, #144523, #169752, .T. ) ;
#14785=CARTESIAN_POINT ( 'NONE',  ( -16.94165728009537020, 66.01213024408822605, -115.6320524760141666 ) ) ;
#14853=ORIENTED_EDGE ( 'NONE', *, *, #148042, .T. ) ;
#15192=ORIENTED_EDGE ( 'NONE', *, *, #64090, .T. ) ;
#15250=CIRCLE ( 'NONE', #227615, 0.09999999999999939493 ) ;
#15312=CARTESIAN_POINT ( 'NONE',  ( 12.26145404764308999, 66.64858632091066681, -119.5427639169754315 ) ) ;
#15483=FACE_OUTER_BOUND ( 'NONE', #1288, .T. ) ;
#15713=LINE ( 'NONE', #109632, #154843 ) ;
#15779=EDGE_CURVE ( 'NONE', #152369, #127414, #103647, .T. ) ;
#15794=ORIENTED_EDGE ( 'NONE', *, *, #13863, .F. ) ;
#15991=DIRECTION ( 'NONE',  ( 1.000000000000000000, 0.000000000000000000, 0.000000000000000000 ) ) ;
#16327=CARTESIAN_POINT ( 'NONE',  ( -12.25000000000000178, 66.15000000001204228, -119.7731074845243739 ) ) ;
#16352=FACE_OUTER_BOUND ( 'NONE', #198885, .T. ) ;
#16417=ORIENTED_EDGE ( 'NONE', *, *, #24137, .F. ) ;
#16436=CARTESIAN_POINT ( 'NONE',  ( -16.81744102076748959, 66.05000000001201954, -115.6731074845243796 ) ) ;
#16485=ORIENTED_EDGE ( 'NONE', *, *, #243562, .F. ) ;
#16531=DIRECTION ( 'NONE',  ( 1.000000000000000000, 0.000000000000000000, 0.000000000000000000 ) ) ;
#16596=CARTESIAN_POINT ( 'NONE',  ( 13.77030915526558630, 66.54399267394271078, -118.0344739903776201 ) ) ;
#16640=CARTESIAN_POINT ( 'NONE',  ( -16.94062896051973865, 66.00728089491138917, -123.9205909424055676 ) ) ;
#16754=EDGE_CURVE ( 'NONE', #208088, #31295, #215595, .T. ) ;
#16766=LINE ( 'NONE', #76705, #28270 ) ;
#16800=VERTEX_POINT ( 'NONE', #95997 ) ;
#16822=CARTESIAN_POINT ( 'NONE',  ( 18.39999999999999503, 70.35000000001207354, -123.8731074845243398 ) ) ;
#16879=CARTESIAN_POINT ( 'NONE',  ( -16.80438519320023616, 66.05022090354371755, -123.8723692036030997 ) ) ;
#16946=EDGE_CURVE ( 'NONE', #242236, #16800, #129375, .T. ) ;
#16974=EDGE_LOOP ( 'NONE', ( #6360, #99811, #232006 ) ) ;
#17089=CARTESIAN_POINT ( 'NONE',  ( -18.40000000000000213, 64.66825945288681510, -115.6731074845243796 ) ) ;
#17090=ORIENTED_EDGE ( 'NONE', *, *, #144136, .F. ) ;
#17103=VECTOR ( 'NONE', #27685, 1000.000000000000000 ) ;
#17182=DIRECTION ( 'NONE',  ( 0.000000000000000000, 6.982962677686266711E-15, -1.000000000000000000 ) ) ;
#17224=EDGE_LOOP ( 'NONE', ( #188080, #172234, #120444, #128689 ) ) ;
#17334=ADVANCED_FACE ( 'NONE', ( #249391 ), #205091, .F. ) ;
#17583=CARTESIAN_POINT ( 'NONE',  ( 18.39999999999999503, 64.25000000001207923, -123.8731074845243683 ) ) ;
#17763=VERTEX_POINT ( 'NONE', #251643 ) ;
#17807=VERTEX_POINT ( 'NONE', #174726 ) ;
#17890=DIRECTION ( 'NONE',  ( 0.000000000000000000, -6.982962677686266711E-15, 1.000000000000000000 ) ) ;
#17897=CARTESIAN_POINT ( 'NONE',  ( 16.87683809663749557, 66.05000000001203375, -115.6731074845243654 ) ) ;
#18157=ORIENTED_EDGE ( 'NONE', *, *, #15779, .F. ) ;
#18298=CARTESIAN_POINT ( 'NONE',  ( -16.78493211734303614, 66.05416425680782311, -115.6870565036283978 ) ) ;
#18379=EDGE_CURVE ( 'NONE', #221298, #239536, #5969, .T. ) ;
#18395=VERTEX_POINT ( 'NONE', #146750 ) ;
#18567=DIRECTION ( 'NONE',  ( -0.000000000000000000, -6.982962677686266711E-15, 1.000000000000000000 ) ) ;
#18579=CARTESIAN_POINT ( 'NONE',  ( 15.48841904831874849, 67.43841904833084300, -123.8731074845243683 ) ) ;
#18713=CARTESIAN_POINT ( 'NONE',  ( 20.27550659511089037, 66.78395627750320784, -123.8731074845243683 ) ) ;
#18982=CARTESIAN_POINT ( 'NONE',  ( -12.30589683808040391, 66.64325398293378555, -119.3197477631602084 ) ) ;
#19263=CARTESIAN_POINT ( 'NONE',  ( 18.39999999999998082, 64.52683809664961245, -127.2731074845243882 ) ) ;
#19374=VERTEX_POINT ( 'NONE', #205506 ) ;
#19377=FACE_OUTER_BOUND ( 'NONE', #52825, .T. ) ;
#19596=CARTESIAN_POINT ( 'NONE',  ( -16.80100914604134132, 66.05685090590840503, -115.7060633572367010 ) ) ;
#19692=CARTESIAN_POINT ( 'NONE',  ( -16.77683809663752257, 66.05416425680785153, -115.6870565036285683 ) ) ;
#19871=VERTEX_POINT ( 'NONE', #13443 ) ;
#20143=CARTESIAN_POINT ( 'NONE',  ( -16.93294127766158752, 65.99671989705713315, -115.5932002186951451 ) ) ;
#20371=CARTESIAN_POINT ( 'NONE',  ( -17.27223548802834685, 65.65460260866079523, -125.1567136637387421 ) ) ;
#20529=LINE ( 'NONE', #179602, #177870 ) ;
#20892=DIRECTION ( 'NONE',  ( -1.073024830501117725E-15, -6.982962677686266711E-15, 1.000000000000000000 ) ) ;
#21186=AXIS2_PLACEMENT_3D ( 'NONE', #165782, #148778, #127924 ) ;
#21209=DIRECTION ( 'NONE',  ( -1.000000000000000000, 0.000000000000000000, 0.000000000000000000 ) ) ;
#21442=CARTESIAN_POINT ( 'NONE',  ( -16.93589915522259304, 65.99137474131613601, -115.5825473825640728 ) ) ;
#21582=ORIENTED_EDGE ( 'NONE', *, *, #52588, .T. ) ;
#21639=CARTESIAN_POINT ( 'NONE',  ( -17.29838795458446654, 65.62845014206513383, -125.1278487671420834 ) ) ;
#21836=UNCERTAINTY_MEASURE_WITH_UNIT (LENGTH_MEASURE( 1.000000000000000082E-05 ), #201303, 'distance_accuracy_value', 'NONE');
#22061=CARTESIAN_POINT ( 'NONE',  ( -17.11825945287482753, 66.05000000001209060, -123.7731074845243597 ) ) ;
#22146=EDGE_CURVE ( 'NONE', #109222, #79626, #178959, .T. ) ;
#22301=DIRECTION ( 'NONE',  ( -1.186688945009010077E-16, -1.000000000000000000, -6.982962677686266711E-15 ) ) ;
#22700=( NAMED_UNIT ( * ) PLANE_ANGLE_UNIT ( ) SI_UNIT ( $, .RADIAN. ) );
#22925=CARTESIAN_POINT ( 'NONE',  ( -16.86379686415369861, 66.02478224075890978, -123.9564973736146527 ) ) ;
#23066=CARTESIAN_POINT ( 'NONE',  ( -16.87851181299898684, 66.04995707600431842, -123.8732509998912832 ) ) ;
#23279=VECTOR ( 'NONE', #173186, 1000.000000000000000 ) ;
#23358=CARTESIAN_POINT ( 'NONE',  ( -18.40000000000000213, 64.51332499825430489, -112.2731074845243739 ) ) ;
#23575=CIRCLE ( 'NONE', #144297, 14.20833333333333748 ) ;
#23766=CARTESIAN_POINT ( 'NONE',  ( -16.92507428761700439, 66.05000000001201954, -115.7365049441459490 ) ) ;
#23825=LINE ( 'NONE', #121634, #249513 ) ;
#24005=CARTESIAN_POINT ( 'NONE',  ( -16.93234230245721861, 66.00189262946491908, -115.6054172028581206 ) ) ;
#24043=CARTESIAN_POINT ( 'NONE',  ( -16.97683809663752186, 66.05000000001201954, -116.4254715027206828 ) ) ;
#24131=VECTOR ( 'NONE', #58990, 1000.000000000000000 ) ;
#24137=EDGE_CURVE ( 'NONE', #191970, #37506, #228420, .T. ) ;
#24452=EDGE_CURVE ( 'NONE', #70684, #256630, #45713, .T. ) ;
#24468=ORIENTED_EDGE ( 'NONE', *, *, #86827, .T. ) ;
#25066=ORIENTED_EDGE ( 'NONE', *, *, #178440, .F. ) ;
#25248=MANIFOLD_SOLID_BREP ( 'Stock-MAS-200-1', #140757 ) ;
#25336=VECTOR ( 'NONE', #49764, 1000.000000000000000 ) ;
#25815=B_SPLINE_CURVE_WITH_KNOTS ( 'NONE', 3,
 ( #170039, #189566, #27945, #29240, #255562, #135653, #70923, #51292, #87855, #215208 ),
 .UNSPECIFIED., .F., .F.,
 ( 4, 3, 3, 4 ),
 ( 1.891637802867244836E-15, 3.877043166999269576E-05, 7.336897548475566824E-05, 7.659383120239756379E-05 ),
 .UNSPECIFIED. ) ;
#25847=ORIENTED_EDGE ( 'NONE', *, *, #4678, .T. ) ;
#25948=B_SPLINE_CURVE_WITH_KNOTS ( 'NONE', 3,
 ( #132064, #34283, #252004, #246863, #248162, #207774, #73407, #49950, #209035, #150357, #229887, #152949, #30412, #232471, #147788, #189479, #133356, #212891, #227305, #48667, #51209, #90358, #130775, #210331, #31715, #254544 ),
 .UNSPECIFIED., .F., .F.,
 ( 4, 2, 2, 2, 2, 2, 2, 2, 2, 2, 2, 2, 4 ),
 ( 0.005476422646581347378, 0.006160811967703578272, 0.006845201288825809166, 0.007187395949386910302, 0.007529590609948011437, 0.007871785270509112573, 0.008213979931070213708, 0.008556174591631314844, 0.008898369252192415979, 0.009240563912753515380, 0.009582758573314618250, 0.01026714789443681879, 0.01095153721555902106 ),
 .UNSPECIFIED. ) ;
#25994=DIRECTION ( 'NONE',  ( 1.186688945009010077E-16, 1.000000000000000000, 6.982962677686266711E-15 ) ) ;
#26053=ADVANCED_FACE ( 'NONE', ( #83612 ), #104472, .F. ) ;
#26162=ORIENTED_EDGE ( 'NONE', *, *, #188336, .T. ) ;
#26408=ORIENTED_EDGE ( 'NONE', *, *, #29729, .F. ) ;
#26440=EDGE_CURVE ( 'NONE', #221298, #241136, #3779, .T. ) ;
#26561=( BOUNDED_SURFACE ( )  B_SPLINE_SURFACE ( 3, 2, ( 
 ( #162445, #103705, #222361 ),
 ( #63309, #198979, #81566 ),
 ( #21639, #20371, #161150 ),
 ( #99848, #2046, #141573 ) ),
 .UNSPECIFIED., .F., .F., .F. ) 
 B_SPLINE_SURFACE_WITH_KNOTS ( ( 4, 4 ),
 ( 3, 3 ),
 ( 5.727910411845712702, 5.983100554402349225 ),
 ( 0.000000000000000000, 1.000000000000000000 ),
 .UNSPECIFIED. ) 
 GEOMETRIC_REPRESENTATION_ITEM ( )  RATIONAL_B_SPLINE_SURFACE ( (
 ( 1.000000000000000000, 0.8946697475932141597, 1.000000000000000000),
 ( 1.000000000000000000, 0.9035312726220684487, 1.000000000000000000),
 ( 1.000000000000000000, 0.9104333467450373973, 1.000000000000000000),
 ( 1.000000000000000000, 0.9152888060719408525, 1.000000000000000000) ) ) 
 REPRESENTATION_ITEM ( '' )  SURFACE ( )  );
#26569=CARTESIAN_POINT ( 'NONE',  ( -16.93521499325732549, 66.00521388020847269, -115.6159989434308244 ) ) ;
#26663=CARTESIAN_POINT ( 'NONE',  ( -13.54795643572458097, 66.54933111084451980, -121.4675609943170116 ) ) ;
#26886=ORIENTED_EDGE ( 'NONE', *, *, #912, .F. ) ;
#26892=ORIENTED_EDGE ( 'NONE', *, *, #16946, .T. ) ;
#26898=LINE ( 'NONE', #221199, #198900 ) ;
#27268=ORIENTED_EDGE ( 'NONE', *, *, #7011, .F. ) ;
#27277=DIRECTION ( 'NONE',  ( 0.2834754621636358940, 0.2834754621636501049, -0.9161240771326873977 ) ) ;
#27632=CARTESIAN_POINT ( 'NONE',  ( -16.97683809663753252, 66.05000000001207638, -123.2515827158544397 ) ) ;
#27685=DIRECTION ( 'NONE',  ( 0.000000000000000000, 6.982962677686266711E-15, -1.000000000000000000 ) ) ;
#27908=CARTESIAN_POINT ( 'NONE',  ( -16.87401514999234209, 66.05000000001201954, -115.7430894919920377 ) ) ;
#27945=CARTESIAN_POINT ( 'NONE',  ( -16.91247567987038636, 66.04091731634281359, -123.8943830259870253 ) ) ;
#27961=CARTESIAN_POINT ( 'NONE',  ( -12.60206096961791999, 66.61031399435634626, -120.8502639781730181 ) ) ;
#28234=AXIS2_PLACEMENT_3D ( 'NONE', #50982, #134378, #249225 ) ;
#28270=VECTOR ( 'NONE', #237080, 1000.000000000000000 ) ;
#28733=ORIENTED_EDGE ( 'NONE', *, *, #255859, .T. ) ;
#28814=VERTEX_POINT ( 'NONE', #158503 ) ;
#28886=FACE_OUTER_BOUND ( 'NONE', #69089, .T. ) ;
#29153=FACE_OUTER_BOUND ( 'NONE', #74772, .T. ) ;
#29240=CARTESIAN_POINT ( 'NONE',  ( -16.92132318717937522, 66.03392997600613512, -123.9007008541722996 ) ) ;
#29286=FACE_OUTER_BOUND ( 'NONE', #152595, .T. ) ;
#29325=EDGE_CURVE ( 'NONE', #41514, #257159, #211202, .T. ) ;
#29475=ORIENTED_EDGE ( 'NONE', *, *, #164104, .F. ) ;
#29507=ORIENTED_EDGE ( 'NONE', *, *, #51974, .T. ) ;
#29729=EDGE_CURVE ( 'NONE', #64566, #12012, #103013, .T. ) ;
#29916=CYLINDRICAL_SURFACE ( 'NONE', #171440, 1.749999999999999778 ) ;
#29976=ORIENTED_EDGE ( 'NONE', *, *, #32691, .F. ) ;
#30013=VERTEX_POINT ( 'NONE', #239666 ) ;
#30152=CARTESIAN_POINT ( 'NONE',  ( -16.88328101497759448, 66.04964716579314654, -115.6719279695950888 ) ) ;
#30385=VERTEX_POINT ( 'NONE', #59386 ) ;
#30412=CARTESIAN_POINT ( 'NONE',  ( 13.88302573338718560, 66.54258905524463330, -121.5230235107343333 ) ) ;
#30505=CARTESIAN_POINT ( 'NONE',  ( -16.97683809663752186, 66.15000000001207070, -123.8731074845243683 ) ) ;
#30516=CARTESIAN_POINT ( 'NONE',  ( -12.93407622233968901, 66.58221053305987880, -121.1657229405475391 ) ) ;
#30748=VERTEX_POINT ( 'NONE', #19692 ) ;
#30877=ORIENTED_EDGE ( 'NONE', *, *, #160740, .F. ) ;
#31126=EDGE_CURVE ( 'NONE', #204362, #32814, #85448, .T. ) ;
#31183=ORIENTED_EDGE ( 'NONE', *, *, #87606, .T. ) ;
#31274=EDGE_LOOP ( 'NONE', ( #249689, #57341, #194975, #8672 ) ) ;
#31287=VECTOR ( 'NONE', #60912, 1000.000000000000000 ) ;
#31295=VERTEX_POINT ( 'NONE', #34026 ) ;
#31452=CARTESIAN_POINT ( 'NONE',  ( -16.88593481969334320, 66.04943990992768477, -115.6712352275798708 ) ) ;
#31524=( BOUNDED_SURFACE ( )  B_SPLINE_SURFACE ( 3, 2, ( 
 ( #38457, #234080, #213228 ),
 ( #172886, #252354, #214517 ),
 ( #76288, #37196, #235364 ),
 ( #112864, #55417, #72469 ) ),
 .UNSPECIFIED., .F., .F., .T. ) 
 B_SPLINE_SURFACE_WITH_KNOTS ( ( 4, 4 ),
 ( 3, 3 ),
 ( 3.658908243880901523, 4.712388980384689674 ),
 ( 0.000000000000000000, 1.000000000000000000 ),
 .UNSPECIFIED. ) 
 GEOMETRIC_REPRESENTATION_ITEM ( )  RATIONAL_B_SPLINE_SURFACE ( (
 ( 1.000000000000000000, 0.8984936768950559927, 1.000000000000000000),
 ( 1.000000000000000000, 0.8646876308615097928, 1.000000000000000000),
 ( 1.000000000000000000, 0.7953136715913377008, 1.000000000000000000),
 ( 1.000000000000000000, 0.7071067811864985009, 1.000000000000000000) ) ) 
 REPRESENTATION_ITEM ( '' )  SURFACE ( )  );
#31567=EDGE_CURVE ( 'NONE', #79398, #98192, #174530, .T. ) ;
#31676=CARTESIAN_POINT ( 'NONE',  ( -17.11825945287482753, 65.95000000001208207, -123.8731074845243683 ) ) ;
#31685=AXIS2_PLACEMENT_3D ( 'NONE', #81689, #157456, #200400 ) ;
#31715=CARTESIAN_POINT ( 'NONE',  ( 15.74999999999999289, 66.65000000001207070, -120.0045385271217526 ) ) ;
#31786=CARTESIAN_POINT ( 'NONE',  ( -16.93301857435212199, 66.02369064527653109, -115.6373319133629423 ) ) ;
#31812=CARTESIAN_POINT ( 'NONE',  ( -12.25000000000000355, 66.65000000001207070, -120.0045385271217384 ) ) ;
#31883=( BOUNDED_CURVE ( )  B_SPLINE_CURVE ( 3, ( #221136, #3365, #46349, #146717 ),
 .UNSPECIFIED., .F., .F. ) 
 B_SPLINE_CURVE_WITH_KNOTS ( ( 4, 4 ),
 ( 0.3000847527772370071, 0.5497968875596834781 ),
 .UNSPECIFIED. ) 
 CURVE ( )  GEOMETRIC_REPRESENTATION_ITEM ( )  RATIONAL_B_SPLINE_CURVE ( ( 1.000000000000000000, 0.9948104011409417691, 0.9948104011409417691, 1.000000000000000000 ) ) 
 REPRESENTATION_ITEM ( '' )  );
#32272=DIRECTION ( 'NONE',  ( 1.000000000000000000, 0.000000000000000000, 0.000000000000000000 ) ) ;
#32501=DIRECTION ( 'NONE',  ( 1.000000000000000000, 0.000000000000000000, 0.000000000000000000 ) ) ;
#32691=EDGE_CURVE ( 'NONE', #256568, #28814, #36301, .T. ) ;
#32757=ORIENTED_EDGE ( 'NONE', *, *, #16754, .T. ) ;
#32814=VERTEX_POINT ( 'NONE', #111984 ) ;
#33026=ORIENTED_EDGE ( 'NONE', *, *, #6350, .T. ) ;
#33098=CARTESIAN_POINT ( 'NONE',  ( -16.89318236219975944, 66.04846474213687202, -115.6679778524185309 ) ) ;
#33186=ORIENTED_EDGE ( 'NONE', *, *, #169118, .F. ) ;
#33205=VERTEX_POINT ( 'NONE', #217150 ) ;
#33372=FACE_OUTER_BOUND ( 'NONE', #66592, .T. ) ;
#34026=CARTESIAN_POINT ( 'NONE',  ( 21.72449340488909897, 65.71604372252087956, -115.6731074845243796 ) ) ;
#34271=AXIS2_PLACEMENT_3D ( 'NONE', #107449, #69626, #245681 ) ;
#34283=CARTESIAN_POINT ( 'NONE',  ( 12.25000000000000000, 66.65000000001202807, -120.0015881126992241 ) ) ;
#34309=EDGE_CURVE ( 'NONE', #256568, #191326, #212095, .T. ) ;
#34366=CARTESIAN_POINT ( 'NONE',  ( -16.92973740335361299, 66.00749618554520737, -115.6170484493226525 ) ) ;
#34508=CARTESIAN_POINT ( 'NONE',  ( -18.40000000000000213, 64.25000000001202238, -115.6731074845243938 ) ) ;
#34517=ORIENTED_EDGE ( 'NONE', *, *, #252271, .T. ) ;
#34528=CARTESIAN_POINT ( 'NONE',  ( -17.01825945287482966, 65.95000000001208207, -123.8731074845243683 ) ) ;
#34654=CARTESIAN_POINT ( 'NONE',  ( -16.87331047859651179, 66.05000000001207638, -123.8731074845243683 ) ) ;
#34763=CARTESIAN_POINT ( 'NONE',  ( -16.87036670365549895, 66.01058118071040326, -124.0026676018264169 ) ) ;
#34876=VECTOR ( 'NONE', #79134, 1000.000000000000000 ) ;
#34888=CARTESIAN_POINT ( 'NONE',  ( 12.33938619321247643, 66.63927620602599688, -119.2091802899176542 ) ) ;
#34940=CARTESIAN_POINT ( 'NONE',  ( -16.94107738177415712, 65.98576071487543970, -123.9731074845243626 ) ) ;
#34959=ADVANCED_FACE ( 'NONE', ( #35779 ), #115287, .F. ) ;
#35185=CARTESIAN_POINT ( 'NONE',  ( -16.79184697841823493, 66.05123833835365588, -123.8689652139218538 ) ) ;
#35212=ORIENTED_EDGE ( 'NONE', *, *, #41132, .T. ) ;
#35261=ORIENTED_EDGE ( 'NONE', *, *, #199743, .F. ) ;
#35471=ORIENTED_EDGE ( 'NONE', *, *, #151758, .T. ) ;
#35534=CARTESIAN_POINT ( 'NONE',  ( -16.80100426158790938, 66.05684947961590581, -123.8401617316903156 ) ) ;
#35619=EDGE_CURVE ( 'NONE', #17763, #154055, #248743, .T. ) ;
#35628=PLANE ( 'NONE',  #176763 ) ;
#35658=CARTESIAN_POINT ( 'NONE',  ( -16.85718274719364373, 66.02385768539031119, -115.5864538167070066 ) ) ;
#35779=FACE_OUTER_BOUND ( 'NONE', #210970, .T. ) ;
#36299=CARTESIAN_POINT ( 'NONE',  ( 23.24999999999999645, 67.17743825834568838, -127.2731074845243597 ) ) ;
#36301=LINE ( 'NONE', #255270, #102556 ) ;
#36326=EDGE_CURVE ( 'NONE', #7208, #198087, #81303, .T. ) ;
#36404=ORIENTED_EDGE ( 'NONE', *, *, #83829, .F. ) ;
#36455=CARTESIAN_POINT ( 'NONE',  ( -16.77683809663752257, 66.05416425680790837, -123.8591584654201512 ) ) ;
#36456=EDGE_CURVE ( 'NONE', #156548, #33205, #75397, .T. ) ;
#36486=EDGE_CURVE ( 'NONE', #44866, #70684, #135502, .T. ) ;
#36844=DIRECTION ( 'NONE',  ( 0.000000000000000000, -6.789366196018718420E-15, 1.000000000000000000 ) ) ;
#36856=ADVANCED_FACE ( 'NONE', ( #69212 ), #168335, .T. ) ;
#36944=CARTESIAN_POINT ( 'NONE',  ( -16.89797118371550511, 66.02361927736761515, -115.5858141169661621 ) ) ;
#37006=ORIENTED_EDGE ( 'NONE', *, *, #24137, .T. ) ;
#37127=ORIENTED_EDGE ( 'NONE', *, *, #199566, .F. ) ;
#37196=CARTESIAN_POINT ( 'NONE',  ( -17.05016517656014940, 66.05000000001014371, -115.6958054805232621 ) ) ;
#37281=CARTESIAN_POINT ( 'NONE',  ( -16.97048361161167662, 66.05000000001203375, -116.1642231400940091 ) ) ;
#37363=CARTESIAN_POINT ( 'NONE',  ( 20.05000000000002913, 68.75000000001206502, -127.2731074845243597 ) ) ;
#37440=CARTESIAN_POINT ( 'NONE',  ( 15.51872946208854920, 66.62341902196808974, -118.8961612375124446 ) ) ;
#37475=EDGE_CURVE ( 'NONE', #130548, #107243, #132338, .T. ) ;
#37487=CARTESIAN_POINT ( 'NONE',  ( -16.94445028196808778, 66.00793639031432747, -123.9157773061059231 ) ) ;
#37506=VERTEX_POINT ( 'NONE', #106057 ) ;
#37791=ORIENTED_EDGE ( 'NONE', *, *, #189869, .T. ) ;
#37888=CARTESIAN_POINT ( 'NONE',  ( -16.81931177881022421, 66.06300394050809643, -115.7498896059071853 ) ) ;
#38018=ORIENTED_EDGE ( 'NONE', *, *, #237023, .F. ) ;
#38091=DIRECTION ( 'NONE',  ( 1.186688945009009831E-16, 1.000000000000000000, 6.982962677686266711E-15 ) ) ;
#38108=FACE_BOUND ( 'NONE', #114635, .T. ) ;
#38303=AXIS2_PLACEMENT_3D ( 'NONE', #71503, #12809, #111904 ) ;
#38457=CARTESIAN_POINT ( 'NONE',  ( -16.87242674293849731, 66.05000000001201954, -115.6720172381520229 ) ) ;
#38560=CARTESIAN_POINT ( 'NONE',  ( -13.77083647240106501, 66.54258906972185628, -118.0231915757780854 ) ) ;
#38763=FACE_OUTER_BOUND ( 'NONE', #16974, .T. ) ;
#38851=ORIENTED_EDGE ( 'NONE', *, *, #151758, .F. ) ;
#39008=CARTESIAN_POINT ( 'NONE',  ( -16.77977881697927032, 66.05339806647916134, -123.8617289114093154 ) ) ;
#39026=ORIENTED_EDGE ( 'NONE', *, *, #7011, .T. ) ;
#39055=EDGE_CURVE ( 'NONE', #107243, #76307, #170611, .T. ) ;
#39174=CARTESIAN_POINT ( 'NONE',  ( -16.85939681242906119, 66.09477481408670485, -115.9831855293328857 ) ) ;
#39531=CARTESIAN_POINT ( 'NONE',  ( -18.40000000000000213, 64.51332499825441857, -127.2731074845243882 ) ) ;
#39641=CARTESIAN_POINT ( 'NONE',  ( -18.40000000000000213, 70.35000000001207354, -123.8731074845243398 ) ) ;
#39698=( NAMED_UNIT ( * ) PLANE_ANGLE_UNIT ( ) SI_UNIT ( $, .RADIAN. ) );
#39978=VERTEX_POINT ( 'NONE', #87843 ) ;
#40129=EDGE_CURVE ( 'NONE', #64183, #3872, #232455, .T. ) ;
#40305=CARTESIAN_POINT ( 'NONE',  ( -18.40000000000000213, 64.25000000001207923, -123.8731074845243683 ) ) ;
#40306=EDGE_CURVE ( 'NONE', #18395, #239536, #143822, .T. ) ;
#40436=EDGE_CURVE ( 'NONE', #175428, #175330, #91425, .T. ) ;
#40741=CARTESIAN_POINT ( 'NONE',  ( 12.25000000000000000, 66.15000000001204228, -119.7731074845243739 ) ) ;
#40766=EDGE_CURVE ( 'NONE', #30748, #13858, #230668, .T. ) ;
#40816=CARTESIAN_POINT ( 'NONE',  ( 20.99999999999999645, 66.25000000001207923, -123.8731074845243683 ) ) ;
#40863=ORIENTED_EDGE ( 'NONE', *, *, #90302, .T. ) ;
#40926=AXIS2_PLACEMENT_3D ( 'NONE', #179007, #197244, #21209 ) ;
#41132=EDGE_CURVE ( 'NONE', #198087, #143067, #67385, .T. ) ;
#41209=CARTESIAN_POINT ( 'NONE',  ( -16.86337532320261801, 66.02003279578769934, -123.9720319535071695 ) ) ;
#41303=CARTESIAN_POINT ( 'NONE',  ( -18.40000000000000213, 67.17743825834557470, -112.2731074845243597 ) ) ;
#41514=VERTEX_POINT ( 'NONE', #183192 ) ;
#41629=CARTESIAN_POINT ( 'NONE',  ( -21.65000000000000213, 68.75000000001202238, -115.6731074845243512 ) ) ;
#41694=EDGE_LOOP ( 'NONE', ( #78101, #126170, #131053 ) ) ;
#41795=CARTESIAN_POINT ( 'NONE',  ( -16.86578989773640913, 66.01519019875320282, -115.5584425979021432 ) ) ;
#42142=AXIS2_PLACEMENT_3D ( 'NONE', #55866, #238377, #157609 ) ;
#42160=ORIENTED_EDGE ( 'NONE', *, *, #152814, .F. ) ;
#42415=CARTESIAN_POINT ( 'NONE',  ( -23.25000000000000355, 64.25000000001210765, -127.2731074845243882 ) ) ;
#42468=FACE_OUTER_BOUND ( 'NONE', #57541, .T. ) ;
#42990=AXIS2_PLACEMENT_3D ( 'NONE', #105280, #206991, #164018 ) ;
#43133=CARTESIAN_POINT ( 'NONE',  ( -16.87683809663752399, 54.76195096157899656, -123.8731074845244393 ) ) ;
#43294=AXIS2_PLACEMENT_3D ( 'NONE', #199520, #20892, #179947 ) ;
#43681=CIRCLE ( 'NONE', #189433, 0.9000000000000014655 ) ;
#44005=CARTESIAN_POINT ( 'NONE',  ( 21.13736287352038445, 67.95335762362800835, -115.6731074845243654 ) ) ;
#44152=ORIENTED_EDGE ( 'NONE', *, *, #224428, .F. ) ;
#44238=VECTOR ( 'NONE', #243546, 999.9999999999998863 ) ;
#44295=CARTESIAN_POINT ( 'NONE',  ( -16.78805706634180339, 66.05174750694081354, -115.6789542764925045 ) ) ;
#44348=CARTESIAN_POINT ( 'NONE',  ( -16.87036670365548474, 66.01058118071036063, -115.5435473672223168 ) ) ;
#44866=VERTEX_POINT ( 'NONE', #188228 ) ;
#44926=CARTESIAN_POINT ( 'NONE',  ( -15.75000000000000355, 66.65000000001204228, -119.7731074845243739 ) ) ;
#45299=ORIENTED_EDGE ( 'NONE', *, *, #144136, .T. ) ;
#45456=CARTESIAN_POINT ( 'NONE',  ( -17.01764560440453877, 66.05000000001209060, -123.7731074853111721 ) ) ;
#45567=CARTESIAN_POINT ( 'NONE',  ( -16.78270389226384296, 66.05262738339500572, -115.6819004476129038 ) ) ;
#45653=( BOUNDED_SURFACE ( )  B_SPLINE_SURFACE ( 3, 2, ( 
 ( #186967, #89118, #129541 ),
 ( #51248, #231224, #249495 ),
 ( #189519, #66988, #69576 ),
 ( #209071, #47409, #9576 ),
 ( #106087, #87810, #147825 ),
 ( #188223, #10880, #48701 ),
 ( #245631, #107392, #90396 ),
 ( #167402, #246899, #169992 ),
 ( #207817, #128258, #130812 ),
 ( #210366, #250757, #91691 ) ),
 .UNSPECIFIED., .F., .F., .T. ) 
 B_SPLINE_SURFACE_WITH_KNOTS ( ( 4, 2, 2, 2, 4 ),
 ( 3, 3 ),
 ( 0.002161241639767785133, 0.002579950749617447234, 0.002789305304542278284, 0.002893982582004694243, 0.002998659859467109768 ),
 ( 0.000000000000000000, 1.000000000000000000 ),
 .UNSPECIFIED. ) 
 GEOMETRIC_REPRESENTATION_ITEM ( )  RATIONAL_B_SPLINE_SURFACE ( (
 ( 1.000000000000000000, 0.7071067811864985009, 1.000000000000000000),
 ( 1.000000000000000000, 0.7632447400663812109, 1.000000000000000000),
 ( 1.000000000000000000, 0.8158073005109720555, 1.000000000000000000),
 ( 1.000000000000000000, 0.8906973462395535446, 1.000000000000000000),
 ( 1.000000000000000000, 0.9149408947797246228, 1.000000000000000000),
 ( 1.000000000000000000, 0.9493368785277208621, 1.000000000000000000),
 ( 1.000000000000000000, 0.9605194247156264575, 1.000000000000000000),
 ( 1.000000000000000000, 0.9803630264781529879, 1.000000000000000000),
 ( 1.000000000000000000, 0.9900844824270880196, 1.000000000000000000),
 ( 1.000000000000000000, 0.9894588281429241849, 1.000000000000000000) ) ) 
 REPRESENTATION_ITEM ( '' )  SURFACE ( )  );
#45713=B_SPLINE_CURVE_WITH_KNOTS ( 'NONE', 3,
 ( #52009, #69047, #148569, #246383, #168173, #205965, #172021 ),
 .UNSPECIFIED., .F., .F.,
 ( 4, 3, 4 ),
 ( 3.469446951953614189E-18, 3.882884552234413058E-05, 5.798605692158429121E-05 ),
 .UNSPECIFIED. ) ;
#45964=ORIENTED_EDGE ( 'NONE', *, *, #232883, .F. ) ;
#46005=ORIENTED_EDGE ( 'NONE', *, *, #40306, .F. ) ;
#46006=ADVANCED_FACE ( 'NONE', ( #8321 ), #45653, .F. ) ;
#46169=FACE_OUTER_BOUND ( 'NONE', #145158, .T. ) ;
#46227=EDGE_CURVE ( 'NONE', #17807, #76307, #48073, .T. ) ;
#46349=CARTESIAN_POINT ( 'NONE',  ( -17.78043020864321022, 65.14640788800639370, -126.1861566502445697 ) ) ;
#46367=ORIENTED_EDGE ( 'NONE', *, *, #205823, .F. ) ;
#46381=DIRECTION ( 'NONE',  ( 1.000000000000000000, 0.000000000000000000, 0.000000000000000000 ) ) ;
#46386=LINE ( 'NONE', #41303, #146879 ) ;
#47031=DIRECTION ( 'NONE',  ( -0.000000000000000000, -6.982962677686266711E-15, 1.000000000000000000 ) ) ;
#47157=FACE_OUTER_BOUND ( 'NONE', #104120, .T. ) ;
#47330=CARTESIAN_POINT ( 'NONE',  ( -16.94445028196808778, 66.00793639031432747, -123.9157773061059231 ) ) ;
#47399=AXIS2_PLACEMENT_3D ( 'NONE', #108854, #188392, #7173 ) ;
#47409=CARTESIAN_POINT ( 'NONE',  ( -16.88705144915409662, 66.05000000001207638, -123.5921288898118036 ) ) ;
#47419=CARTESIAN_POINT ( 'NONE',  ( -16.87683809663752399, 66.15000000001201386, -116.4254715027206828 ) ) ;
#47426=COLOUR_RGB ( '', 0.31764706, 0.68627451, 0.89019608) ;
#47465=CARTESIAN_POINT ( 'NONE',  ( -14.87779219673429054, 66.56936653093923439, -121.2913416897003032 ) ) ;
#47820=ORIENTED_EDGE ( 'NONE', *, *, #243430, .F. ) ;
#47967=ORIENTED_EDGE ( 'NONE', *, *, #26440, .F. ) ;
#48016=CARTESIAN_POINT ( 'NONE',  ( -16.87242674293850087, 66.05000000001209060, -123.8741977308967250 ) ) ;
#48073=LINE ( 'NONE', #147174, #101469 ) ;
#48399=LINE ( 'NONE', #161963, #158231 ) ;
#48460=CARTESIAN_POINT ( 'NONE',  ( 13.99999999999999822, 66.15000000001204228, -119.7731074845243739 ) ) ;
#48619=ORIENTED_EDGE ( 'NONE', *, *, #171384, .F. ) ;
#48647=VECTOR ( 'NONE', #177273, 1000.000000000000000 ) ;
#48652=VECTOR ( 'NONE', #232045, 1000.000000000000000 ) ;
#48667=CARTESIAN_POINT ( 'NONE',  ( 15.06592377766031099, 66.58221053305985038, -121.1657229405474681 ) ) ;
#48701=CARTESIAN_POINT ( 'NONE',  ( -16.83233564386414116, 66.06977820342736152, -123.7476281479999898 ) ) ;
#48764=CARTESIAN_POINT ( 'NONE',  ( -13.12432614554023580, 66.56923500458974274, -121.2925700897739603 ) ) ;
#48848=CARTESIAN_POINT ( 'NONE',  ( -16.77683809663752257, 52.34166666667870516, -119.7731074845244592 ) ) ;
#48850=EDGE_LOOP ( 'NONE', ( #181176, #99477, #60832, #146068, #102356 ) ) ;
#48990=CARTESIAN_POINT ( 'NONE',  ( -16.97683809663752186, 66.05000000001203375, -116.4254715027206828 ) ) ;
#49000=CARTESIAN_POINT ( 'NONE',  ( -23.25000000000000355, 66.05000000001210481, -127.2731074845243597 ) ) ;
#49013=AXIS2_PLACEMENT_3D ( 'NONE', #80268, #159862, #60722 ) ;
#49534=AXIS2_PLACEMENT_3D ( 'NONE', #39641, #93150, #154457 ) ;
#49570=CARTESIAN_POINT ( 'NONE',  ( -18.34804628011471195, 64.52683809664971193, -127.2731074845243882 ) ) ;
#49764=DIRECTION ( 'NONE',  ( 0.000000000000000000, -1.000000000000000000, -6.982962677686266711E-15 ) ) ;
#49915=CARTESIAN_POINT ( 'NONE',  ( -17.71734398241073905, 65.15764277154742956, -113.2979692315187918 ) ) ;
#49941=EDGE_CURVE ( 'NONE', #130548, #44866, #253501, .T. ) ;
#49950=CARTESIAN_POINT ( 'NONE',  ( 13.12220780326572012, 66.56936653093924861, -121.2913416897002890 ) ) ;
#50028=PLANE ( 'NONE',  #127752 ) ;
#50113=SURFACE_STYLE_FILL_AREA ( #110090 ) ;
#50327=VECTOR ( 'NONE', #180525, 1000.000000000000000 ) ;
#50418=CARTESIAN_POINT ( 'NONE',  ( -16.86445178670652467, 66.03778837089606668, -123.9138849226416568 ) ) ;
#50787=ORIENTED_EDGE ( 'NONE', *, *, #75327, .T. ) ;
#50920=VECTOR ( 'NONE', #110596, 1000.000000000000000 ) ;
#50982=CARTESIAN_POINT ( 'NONE',  ( 23.04999999999999716, 67.17743825834560312, -115.6731074845243654 ) ) ;
#51209=CARTESIAN_POINT ( 'NONE',  ( 15.15590539855245744, 66.58931770574409370, -121.0919640425760804 ) ) ;
#51212=VERTEX_POINT ( 'NONE', #19263 ) ;
#51248=CARTESIAN_POINT ( 'NONE',  ( -16.97683810757273193, 66.05000000001207638, -123.2595307720638971 ) ) ;
#51292=CARTESIAN_POINT ( 'NONE',  ( -16.94333152886235894, 66.00965798856158528, -123.9151390155787880 ) ) ;
#51354=LINE ( 'NONE', #224876, #73577 ) ;
#51664=ORIENTED_EDGE ( 'NONE', *, *, #255859, .F. ) ;
#51762=CIRCLE ( 'NONE', #85073, 1.749999999999998002 ) ;
#51825=DIRECTION ( 'NONE',  ( 1.186688945009010077E-16, 1.000000000000000000, 6.982962677686266711E-15 ) ) ;
#51974=EDGE_CURVE ( 'NONE', #17807, #150586, #158215, .T. ) ;
#52009=CARTESIAN_POINT ( 'NONE',  ( -18.34374000495059676, 64.52683809664949877, -112.2731074845243739 ) ) ;
#52234=CARTESIAN_POINT ( 'NONE',  ( 20.99999999999999645, 66.25000000001207923, -123.8731074845243683 ) ) ;
#52434=VECTOR ( 'NONE', #172482, 1000.000000000000000 ) ;
#52588=EDGE_CURVE ( 'NONE', #79626, #79879, #159667, .T. ) ;
#52604=CARTESIAN_POINT ( 'NONE',  ( -16.92570016628983609, 66.04121104227213834, -115.6437581545634004 ) ) ;
#52621=EDGE_CURVE ( 'NONE', #182212, #191326, #69271, .T. ) ;
#52825=EDGE_LOOP ( 'NONE', ( #46367, #166715, #170857, #122128 ) ) ;
#52876=DIRECTION ( 'NONE',  ( 0.000000000000000000, 1.000000000000000000, 0.000000000000000000 ) ) ;
#53420=CARTESIAN_POINT ( 'NONE',  ( -16.79814274880124358, 66.05072745733475870, -123.8706744474763752 ) ) ;
#53487=ADVANCED_FACE ( 'NONE', ( #208976 ), #128165, .T. ) ;
#53705=ORIENTED_EDGE ( 'NONE', *, *, #199566, .T. ) ;
#53848=ORIENTED_EDGE ( 'NONE', *, *, #37475, .F. ) ;
#54147=LINE ( 'NONE', #17583, #188584 ) ;
#54165=DIRECTION ( 'NONE',  ( -1.020425574104004196E-15, -6.982962677686266711E-15, 1.000000000000000000 ) ) ;
#54185=ORIENTED_EDGE ( 'NONE', *, *, #912, .T. ) ;
#54317=ORIENTED_EDGE ( 'NONE', *, *, #75327, .F. ) ;
#54412=CARTESIAN_POINT ( 'NONE',  ( 15.57250062127604018, 66.62931007840943209, -118.9966423578633368 ) ) ;
#54461=CARTESIAN_POINT ( 'NONE',  ( -16.94037747912386394, 65.98646061752573644, -123.9719765265488718 ) ) ;
#54791=ADVANCED_FACE ( 'NONE', ( #98026 ), #177631, .F. ) ;
#54839=DIRECTION ( 'NONE',  ( -0.000000000000000000, -6.982962677686266711E-15, 1.000000000000000000 ) ) ;
#54864=CARTESIAN_POINT ( 'NONE',  ( -18.40000000000000213, 64.52683809664949877, -112.3490535513323323 ) ) ;
#54922=ORIENTED_EDGE ( 'NONE', *, *, #242174, .T. ) ;
#55034=CARTESIAN_POINT ( 'NONE',  ( -16.78493832629887095, 66.05416425680792258, -123.8591584654201512 ) ) ;
#55417=CARTESIAN_POINT ( 'NONE',  ( -17.11825945287482043, 66.05000000001203375, -115.6731074845243796 ) ) ;
#55423=CARTESIAN_POINT ( 'NONE',  ( -16.27683809663751191, 66.65000000001209912, -127.2731074845243882 ) ) ;
#55429=CARTESIAN_POINT ( 'NONE',  ( -23.25000000000000355, 70.35000000001207354, -123.8731074845243398 ) ) ;
#55681=VERTEX_POINT ( 'NONE', #163519 ) ;
#55696=LINE ( 'NONE', #214808, #34876 ) ;
#55712=EDGE_LOOP ( 'NONE', ( #239425, #253349, #230194, #206179 ) ) ;
#55866=CARTESIAN_POINT ( 'NONE',  ( 23.04999999999999716, 67.17743825834568838, -127.2731074845243597 ) ) ;
#56029=B_SPLINE_CURVE_WITH_KNOTS ( 'NONE', 3,
 ( #37487, #171887, #212276, #16640, #135268, #113157, #14074, #115726, #192702, #177014, #213528, #133996, #174469, #117009, #253934, #93594, #255171, #54461, #34940 ),
 .UNSPECIFIED., .F., .F.,
 ( 4, 3, 3, 3, 3, 3, 4 ),
 ( 0.0001624081864585828479, 0.0001685232196531679001, 0.0001764526673566893435, 0.0001916878551483146103, 0.0002009890782182573881, 0.0002238845907555200366, 0.0002283406619926361904 ),
 .UNSPECIFIED. ) ;
#56088=EDGE_CURVE ( 'NONE', #256392, #187202, #43681, .T. ) ;
#56104=VERTEX_POINT ( 'NONE', #229615 ) ;
#56269=FACE_OUTER_BOUND ( 'NONE', #166520, .T. ) ;
#56349=LINE ( 'NONE', #75941, #125959 ) ;
#56463=EDGE_CURVE ( 'NONE', #56104, #30748, #143625, .T. ) ;
#56518=VECTOR ( 'NONE', #13365, 1000.000000000000000 ) ;
#56662=EDGE_CURVE ( 'NONE', #120700, #127391, #96931, .T. ) ;
#56782=ADVANCED_FACE ( 'NONE', ( #134172 ), #152493, .F. ) ;
#56786=CARTESIAN_POINT ( 'NONE',  ( -16.92989507731676113, 66.05000000001201954, -115.9056085539141492 ) ) ;
#56974=ADVANCED_FACE ( 'NONE', ( #19377 ), #178474, .F. ) ;
#57099=EDGE_CURVE ( 'NONE', #31295, #12012, #165298, .T. ) ;
#57341=ORIENTED_EDGE ( 'NONE', *, *, #4620, .T. ) ;
#57541=EDGE_LOOP ( 'NONE', ( #175933, #198333, #141946, #78087, #209189 ) ) ;
#58059=CARTESIAN_POINT ( 'NONE',  ( -18.39999999999999858, 64.52683809664961245, -127.1971614177164156 ) ) ;
#58092=CARTESIAN_POINT ( 'NONE',  ( -12.26136940704871670, 66.64859682587037071, -119.5435770476859005 ) ) ;
#58278=DIRECTION ( 'NONE',  ( 0.000000000000000000, -1.000000000000000000, -6.982962677686266711E-15 ) ) ;
#58534=CARTESIAN_POINT ( 'NONE',  ( -16.81744102076749314, 66.05000000001207638, -123.8731074845243683 ) ) ;
#58540=DIRECTION ( 'NONE',  ( 0.7071067811865463515, -0.7071067811865487940, -5.696443396193425170E-15 ) ) ;
#58682=DIRECTION ( 'NONE',  ( 0.7071067811865214825, -0.7071067811865735520, 0.000000000000000000 ) ) ;
#58904=DIRECTION ( 'NONE',  ( -1.000000000000000000, 1.646408749285563322E-14, -1.073024830501002749E-15 ) ) ;
#58990=DIRECTION ( 'NONE',  ( 1.000000000000000000, 0.000000000000000000, 0.000000000000000000 ) ) ;
#59029=CARTESIAN_POINT ( 'NONE',  ( -18.40000000000000213, 70.35000000001201670, -115.6731074845243370 ) ) ;
#59386=CARTESIAN_POINT ( 'NONE',  ( 18.39999999999999503, 64.52683809664958403, -123.8731074845243683 ) ) ;
#59557=CARTESIAN_POINT ( 'NONE',  ( -16.87383368123029825, 66.05000000001207638, -123.8731074845243683 ) ) ;
#59721=EDGE_LOOP ( 'NONE', ( #187197, #135837, #78354, #66955 ) ) ;
#60294=CARTESIAN_POINT ( 'NONE',  ( -33.72168855820451938, 66.05000000001200533, -115.6731074845243228 ) ) ;
#60610=CARTESIAN_POINT ( 'NONE',  ( -15.75000000000000000, 66.65000000001204228, -120.0015881126992525 ) ) ;
#60616=LINE ( 'NONE', #80156, #93147 ) ;
#60721=ORIENTED_EDGE ( 'NONE', *, *, #128761, .T. ) ;
#60722=DIRECTION ( 'NONE',  ( 1.000000000000000000, 0.000000000000000000, 0.000000000000000000 ) ) ;
#60832=ORIENTED_EDGE ( 'NONE', *, *, #120799, .T. ) ;
#60856=ADVANCED_FACE ( 'NONE', ( #130862 ), #149171, .F. ) ;
#60912=DIRECTION ( 'NONE',  ( 0.000000000000000000, 6.982962677686266711E-15, -1.000000000000000000 ) ) ;
#60921=ADVANCED_FACE ( 'NONE', ( #106147 ), #8364, .F. ) ;
#60937=ADVANCED_FACE ( 'NONE', ( #185711 ), #227394, .T. ) ;
#60985=ADVANCED_FACE ( 'NONE', ( #137275 ), #237564, .T. ) ;
#61442=CARTESIAN_POINT ( 'NONE',  ( 18.39999999999998082, 64.52683809664961245, -127.2731074845243882 ) ) ;
#61656=AXIS2_PLACEMENT_3D ( 'NONE', #190066, #207065, #248761 ) ;
#62065=DIRECTION ( 'NONE',  ( 0.000000000000000000, -0.9553114395362733990, 0.2956011730205631016 ) ) ;
#62436=CARTESIAN_POINT ( 'NONE',  ( -33.72168855820451938, 66.05000000001206217, -123.8731074845244251 ) ) ;
#62583=B_SPLINE_CURVE_WITH_KNOTS ( 'NONE', 3,
 ( #132025, #55034, #233710, #35534, #137162, #115034, #254512, #75910, #211572, #176316, #255784, #216697, #203560, #104429 ),
 .UNSPECIFIED., .F., .F.,
 ( 4, 2, 2, 2, 2, 2, 4 ),
 ( 0.000000000000000000, 2.389617747640127089E-05, 4.779235495280254178E-05, 9.558470990564673048E-05, 0.0001911694198113693551, 0.0003823388396228073944, 0.0007646776792456835272 ),
 .UNSPECIFIED. ) ;
#62844=ORIENTED_EDGE ( 'NONE', *, *, #132850, .T. ) ;
#63108=CARTESIAN_POINT ( 'NONE',  ( 16.87683809663749557, 66.05000000001203375, -115.6731074845243654 ) ) ;
#63149=B_SPLINE_CURVE_WITH_KNOTS ( 'NONE', 3,
 ( #134723, #214286, #240277, #39531 ),
 .UNSPECIFIED., .F., .F.,
 ( 4, 4 ),
 ( 0.000000000000000000, 7.713889350930586977E-05 ),
 .UNSPECIFIED. ) ;
#63309=CARTESIAN_POINT ( 'NONE',  ( -17.80356949363974195, 65.12326860300986198, -126.2361805087511328 ) ) ;
#63398=CARTESIAN_POINT ( 'NONE',  ( 18.54999999999999716, 67.25000000001205080, -127.2731074845243597 ) ) ;
#63412=DIRECTION ( 'NONE',  ( -0.000000000000000000, -6.982962677686266711E-15, 1.000000000000000000 ) ) ;
#63433=DIRECTION ( 'NONE',  ( 0.000000000000000000, 0.000000000000000000, 1.000000000000000000 ) ) ;
#63642=CARTESIAN_POINT ( 'NONE',  ( -17.11825945287481332, 65.95000000001201101, -115.7731074845243597 ) ) ;
#64090=EDGE_CURVE ( 'NONE', #76307, #19374, #126903, .T. ) ;
#64183=VERTEX_POINT ( 'NONE', #109173 ) ;
#64438=CARTESIAN_POINT ( 'NONE',  ( -16.87333278164152972, 66.11739021543316142, -116.1562752906778542 ) ) ;
#64442=DIRECTION ( 'NONE',  ( 1.186688945009010077E-16, 1.000000000000000000, 6.982962677686266711E-15 ) ) ;
#64461=LINE ( 'NONE', #206533, #66257 ) ;
#64521=AXIS2_PLACEMENT_3D ( 'NONE', #48848, #128395, #188365 ) ;
#64566=VERTEX_POINT ( 'NONE', #94130 ) ;
#65430=CARTESIAN_POINT ( 'NONE',  ( -16.86132326855785735, 66.05000000001209060, -123.8244716998560619 ) ) ;
#65432=ORIENTED_EDGE ( 'NONE', *, *, #128157, .F. ) ;
#65606=ORIENTED_EDGE ( 'NONE', *, *, #34309, .T. ) ;
#65714=CARTESIAN_POINT ( 'NONE',  ( -16.82055514392360607, 66.05000000001200533, -115.6999055590665932 ) ) ;
#66137=CARTESIAN_POINT ( 'NONE',  ( 18.39999999999999503, 70.35000000001207354, -123.8731074845243398 ) ) ;
#66191=AXIS2_PLACEMENT_3D ( 'NONE', #116360, #15991, #36844 ) ;
#66203=CARTESIAN_POINT ( 'NONE',  ( 21.72449340488910607, 65.71604372252089377, -115.6731074845243796 ) ) ;
#66257=VECTOR ( 'NONE', #186994, 1000.000000000000000 ) ;
#66496=CARTESIAN_POINT ( 'NONE',  ( 18.39999999999999503, 64.25000000001199396, -112.2731074845243739 ) ) ;
#66592=EDGE_LOOP ( 'NONE', ( #214714, #133351, #166464 ) ) ;
#66645=CARTESIAN_POINT ( 'NONE',  ( -20.65000000000000568, 68.75000000001202238, -115.6731074845243512 ) ) ;
#66695=CARTESIAN_POINT ( 'NONE',  ( -16.89146115310546037, 66.04855675435554474, -115.6682850655701600 ) ) ;
#66758=EDGE_CURVE ( 'NONE', #256392, #208088, #26898, .T. ) ;
#66849=VERTEX_POINT ( 'NONE', #48990 ) ;
#66898=DIRECTION ( 'NONE',  ( -1.000000000000000000, 0.000000000000000000, 0.000000000000000000 ) ) ;
#66950=ORIENTED_EDGE ( 'NONE', *, *, #167658, .F. ) ;
#66955=ORIENTED_EDGE ( 'NONE', *, *, #16946, .F. ) ;
#66957=CARTESIAN_POINT ( 'NONE',  ( -16.93860193097148326, 66.00689223268274475, -115.6229691172175222 ) ) ;
#66959=CIRCLE ( 'NONE', #314, 0.9000000000000014655 ) ;
#66988=CARTESIAN_POINT ( 'NONE',  ( -16.89935556175729658, 66.05000000001207638, -123.3834311216395463 ) ) ;
#66999=CARTESIAN_POINT ( 'NONE',  ( -16.83558968593868954, 66.05000000001201954, -115.6854126721413110 ) ) ;
#67002=AXIS2_PLACEMENT_3D ( 'NONE', #205511, #3458, #63433 ) ;
#67385=LINE ( 'NONE', #162645, #191317 ) ;
#67571=PLANE ( 'NONE',  #71181 ) ;
#67622=( BOUNDED_CURVE ( )  B_SPLINE_CURVE ( 3, ( #209215, #147526, #148825, #168427 ),
 .UNSPECIFIED., .F., .F. ) 
 B_SPLINE_CURVE_WITH_KNOTS ( ( 4, 4 ),
 ( 5.731445031868798168, 5.983100554402349225 ),
 .UNSPECIFIED. ) 
 CURVE ( )  GEOMETRIC_REPRESENTATION_ITEM ( )  RATIONAL_B_SPLINE_CURVE ( ( 1.000000000000000000, 0.9947294176030464508, 0.9947294176030464508, 1.000000000000000000 ) ) 
 REPRESENTATION_ITEM ( '' )  );
#67770=B_SPLINE_CURVE_WITH_KNOTS ( 'NONE', 3,
 ( #207504, #148805, #210066, #30152, #31452, #86222, #125388, #66695, #244031, #229622 ),
 .UNSPECIFIED., .F., .F.,
 ( 4, 3, 3, 4 ),
 ( 0.000000000000000000, 1.004626015991719593E-05, 1.831183478183680716E-05, 2.062343583996558100E-05 ),
 .UNSPECIFIED. ) ;
#67797=ORIENTED_EDGE ( 'NONE', *, *, #13507, .T. ) ;
#67932=EDGE_CURVE ( 'NONE', #182212, #257159, #4175, .T. ) ;
#68046=ORIENTED_EDGE ( 'NONE', *, *, #93395, .F. ) ;
#68173=EDGE_CURVE ( 'NONE', #12012, #191970, #140616, .T. ) ;
#68294=CARTESIAN_POINT ( 'NONE',  ( -16.77431908686106610, 66.05419424549403118, -115.6872682668741277 ) ) ;
#68334=DIRECTION ( 'NONE',  ( -1.000000000000000000, 0.000000000000000000, 0.000000000000000000 ) ) ;
#68346=CARTESIAN_POINT ( 'NONE',  ( -15.15766958671843589, 66.58946139148316945, -121.0904194873834285 ) ) ;
#68360=ORIENTED_EDGE ( 'NONE', *, *, #126211, .F. ) ;
#68406=FILL_AREA_STYLE_COLOUR ( '', #47426 ) ;
#68805=DIRECTION ( 'NONE',  ( 0.000000000000000000, -1.000000000000000000, -6.982962677686266711E-15 ) ) ;
#69047=CARTESIAN_POINT ( 'NONE',  ( -18.35668295345803713, 64.52683809664951298, -112.2731074845243739 ) ) ;
#69089=EDGE_LOOP ( 'NONE', ( #101005, #211699, #8919, #141592, #105836 ) ) ;
#69212=FACE_OUTER_BOUND ( 'NONE', #154191, .T. ) ;
#69271=( BOUNDED_CURVE ( )  B_SPLINE_CURVE ( 3, ( #63108, #243039, #200072, #162248 ),
 .UNSPECIFIED., .F., .F. ) 
 B_SPLINE_CURVE_WITH_KNOTS ( ( 4, 4 ),
 ( 3.432212674861197854, 3.693332928900581624 ),
 .UNSPECIFIED. ) 
 CURVE ( )  GEOMETRIC_REPRESENTATION_ITEM ( )  RATIONAL_B_SPLINE_CURVE ( ( 1.000000000000000000, 0.9943260843901262636, 0.9943260843901262636, 1.000000000000000000 ) ) 
 REPRESENTATION_ITEM ( '' )  );
#69296=AXIS2_PLACEMENT_3D ( 'NONE', #241971, #122030, #62065 ) ;
#69327=ORIENTED_EDGE ( 'NONE', *, *, #148271, .F. ) ;
#69576=CARTESIAN_POINT ( 'NONE',  ( -16.87333278164142669, 66.11739021543317563, -123.3899396783716895 ) ) ;
#69626=DIRECTION ( 'NONE',  ( 0.8049926720990051576, -0.5932847527679298016, -4.142885285818778274E-15 ) ) ;
#69910=DIRECTION ( 'NONE',  ( 1.000000000000000000, -1.541976423090492636E-14, 0.000000000000000000 ) ) ;
#70026=ORIENTED_EDGE ( 'NONE', *, *, #165015, .T. ) ;
#70033=CARTESIAN_POINT ( 'NONE',  ( -16.92778301347232883, 65.99905508317726799, -123.9516255924936274 ) ) ;
#70160=CARTESIAN_POINT ( 'NONE',  ( -14.00000000000000178, 66.15000000001204228, -119.7731074845243739 ) ) ;
#70425=CIRCLE ( 'NONE', #120483, 0.1000000000000028644 ) ;
#70684=VERTEX_POINT ( 'NONE', #99496 ) ;
#70790=DIRECTION ( 'NONE',  ( 0.000000000000000000, -1.000000000000000000, -6.837150591533219968E-15 ) ) ;
#70791=LINE ( 'NONE', #128172, #52434 ) ;
#70799=CARTESIAN_POINT ( 'NONE',  ( -17.22361732159831504, 65.65484434140957148, -114.3938920103915109 ) ) ;
#70898=FACE_OUTER_BOUND ( 'NONE', #201632, .T. ) ;
#70923=CARTESIAN_POINT ( 'NONE',  ( -16.94275863009466576, 66.01050395134967630, -123.9148048665654898 ) ) ;
#71181=AXIS2_PLACEMENT_3D ( 'NONE', #147092, #90979, #226631 ) ;
#71252=DIRECTION ( 'NONE',  ( 0.000000000000000000, 6.982962677686266711E-15, -1.000000000000000000 ) ) ;
#71342=ORIENTED_EDGE ( 'NONE', *, *, #36326, .T. ) ;
#71503=CARTESIAN_POINT ( 'NONE',  ( 20.73486653747088582, 68.75000000001205080, -127.2731074845243597 ) ) ;
#71662=DIRECTION ( 'NONE',  ( -1.000000000000000000, 7.492892343619937423E-30, -1.073024830501117725E-15 ) ) ;
#71714=DIRECTION ( 'NONE',  ( -0.000000000000000000, -6.982962677686266711E-15, 1.000000000000000000 ) ) ;
#71724=LINE ( 'NONE', #151260, #86367 ) ;
#71776=CARTESIAN_POINT ( 'NONE',  ( 23.04999999999999716, 67.17743825834568838, -127.2731074845243597 ) ) ;
#71801=DIRECTION ( 'NONE',  ( 0.000000000000000000, -1.000000000000000000, -6.982962677686266711E-15 ) ) ;
#71807=PRODUCT_CONTEXT ( 'NONE', #195588, 'mechanical' ) ;
#71986=CARTESIAN_POINT ( 'NONE',  ( 18.39999999999997371, 64.25000000001210765, -127.2731074845243882 ) ) ;
#72015=PLANE ( 'NONE',  #187700 ) ;
#72037=DIRECTION ( 'NONE',  ( -1.000000000000000000, 0.000000000000000000, -0.000000000000000000 ) ) ;
#72092=ORIENTED_EDGE ( 'NONE', *, *, #165015, .F. ) ;
#72445=ORIENTED_EDGE ( 'NONE', *, *, #166863, .T. ) ;
#72469=CARTESIAN_POINT ( 'NONE',  ( -17.11825945287481687, 65.95000000001201101, -115.6731074845243796 ) ) ;
#72567=CARTESIAN_POINT ( 'NONE',  ( -15.73854595235692244, 66.64858632091065260, -119.5427639169754315 ) ) ;
#72765=CARTESIAN_POINT ( 'NONE',  ( -16.93433913041102912, 65.99402157848805928, -115.5877420571292049 ) ) ;
#72935=DIRECTION ( 'NONE',  ( -1.000000000000000000, -1.652117596168391700E-15, -1.153667551319263085E-29 ) ) ;
#73003=CARTESIAN_POINT ( 'NONE',  ( 20.73486653747090003, 68.75000000001196554, -115.6731074845243512 ) ) ;
#73167=CARTESIAN_POINT ( 'NONE',  ( -23.25000000000000355, 64.25000000001207923, -123.8731074845243683 ) ) ;
#73407=CARTESIAN_POINT ( 'NONE',  ( 12.93225390519045170, 66.58234804117104488, -121.1643200920839263 ) ) ;
#73451=SHAPE_REPRESENTATION ( 'Snap Open Cable Crossbars 13', ( #2425 ), #227278 ) ;
#73457=ORIENTED_EDGE ( 'NONE', *, *, #39055, .T. ) ;
#73577=VECTOR ( 'NONE', #107508, 1000.000000000000000 ) ;
#73815=ADVANCED_FACE ( 'NONE', ( #145785 ), #226602, .F. ) ;
#73851=CARTESIAN_POINT ( 'NONE',  ( -16.97683809663752186, 66.05000000001203375, -116.4254715027206828 ) ) ;
#73894=FACE_OUTER_BOUND ( 'NONE', #59721, .T. ) ;
#74019=CARTESIAN_POINT ( 'NONE',  ( 12.68104795156995124, 66.60346600605809897, -118.6171677053510791 ) ) ;
#74121=CARTESIAN_POINT ( 'NONE',  ( -21.64999999999999858, 66.65000000001207070, -123.8731074845243683 ) ) ;
#74172=VECTOR ( 'NONE', #98070, 999.9999999999998863 ) ;
#74340=CARTESIAN_POINT ( 'NONE',  ( 12.25000000000000000, 66.65000000001204228, -119.7731074845243739 ) ) ;
#74513=ORIENTED_EDGE ( 'NONE', *, *, #18379, .T. ) ;
#74514=EDGE_LOOP ( 'NONE', ( #31183, #216888 ) ) ;
#74523=CARTESIAN_POINT ( 'NONE',  ( -16.86420534634261514, 66.02938455442028953, -115.6047709352869788 ) ) ;
#74770=CARTESIAN_POINT ( 'NONE',  ( -16.89268316805465986, 66.04827818676982076, -115.6673550059788340 ) ) ;
#74772=EDGE_LOOP ( 'NONE', ( #26892, #192238, #74513, #33026, #152715, #109847, #54922, #92387, #120137, #257846, #35471, #175950, #157568, #176095, #7105, #254893, #68046, #174929 ) ) ;
#75146=CARTESIAN_POINT ( 'NONE',  ( -14.11361717019515893, 66.54257354752313347, -118.0230656161243274 ) ) ;
#75196=AXIS2_PLACEMENT_3D ( 'NONE', #169087, #170383, #71252 ) ;
#75327=EDGE_CURVE ( 'NONE', #9830, #109222, #182238, .T. ) ;
#75344=PLANE ( 'NONE',  #154868 ) ;
#75397=( BOUNDED_CURVE ( )  B_SPLINE_CURVE ( 3, ( #31676, #168642, #227265, #47330 ),
 .UNSPECIFIED., .F., .T. ) 
 B_SPLINE_CURVE_WITH_KNOTS ( ( 4, 4 ),
 ( 4.712388980384690562, 5.672655318024762749 ),
 .UNSPECIFIED. ) 
 CURVE ( )  GEOMETRIC_REPRESENTATION_ITEM ( )  RATIONAL_B_SPLINE_CURVE ( ( 1.000000000000000000, 0.9246222802177245237, 0.9246222802177245237, 1.000000000000000000 ) ) 
 REPRESENTATION_ITEM ( '' )  );
#75409=CIRCLE ( 'NONE', #67002, 0.1000000000000028644 ) ;
#75726=AXIS2_PLACEMENT_3D ( 'NONE', #117631, #237586, #199762 ) ;
#75731=ORIENTED_EDGE ( 'NONE', *, *, #35619, .F. ) ;
#75910=CARTESIAN_POINT ( 'NONE',  ( -16.83199030136657370, 66.06935196689859424, -123.7507064618668977 ) ) ;
#75941=CARTESIAN_POINT ( 'NONE',  ( 18.39999999999999503, 64.52683809664949877, -112.2731074845243739 ) ) ;
#75954=EDGE_LOOP ( 'NONE', ( #240681, #188339, #14584, #205576 ) ) ;
#76288=CARTESIAN_POINT ( 'NONE',  ( -17.01764560440361862, 66.05000000001201954, -115.7731074837375616 ) ) ;
#76307=VERTEX_POINT ( 'NONE', #178451 ) ;
#76368=CARTESIAN_POINT ( 'NONE',  ( -16.90138253750127006, 66.05000000001201954, -115.8115447766197974 ) ) ;
#76378=CARTESIAN_POINT ( 'NONE',  ( -13.54036565897075484, 66.54845833862648874, -118.0692319856938184 ) ) ;
#76537=CARTESIAN_POINT ( 'NONE',  ( 12.93279065517212345, 66.58230930894892197, -118.3815067877597897 ) ) ;
#76654=ORIENTED_EDGE ( 'NONE', *, *, #22146, .F. ) ;
#76705=CARTESIAN_POINT ( 'NONE',  ( -16.27683809663750480, 66.65000000001201386, -115.5731074845243711 ) ) ;
#76751=ORIENTED_EDGE ( 'NONE', *, *, #255895, .T. ) ;
#76763=LINE ( 'NONE', #158902, #255310 ) ;
#77041=ORIENTED_EDGE ( 'NONE', *, *, #230058, .F. ) ;
#77191=ORIENTED_EDGE ( 'NONE', *, *, #66758, .T. ) ;
#77345=AXIS2_PLACEMENT_3D ( 'NONE', #16822, #213714, #71662 ) ;
#77378=ADVANCED_FACE ( 'NONE', ( #79343 ), #216295, .F. ) ;
#77643=CARTESIAN_POINT ( 'NONE',  ( -16.97683809663755028, 66.05000000001204796, -116.2946366524138142 ) ) ;
#77658=CARTESIAN_POINT ( 'NONE',  ( -15.39126916658603150, 66.61042836546560864, -118.7054667721551766 ) ) ;
#77703=ORIENTED_EDGE ( 'NONE', *, *, #144210, .T. ) ;
#77729=DIRECTION ( 'NONE',  ( -1.073024830501117725E-15, 6.982962677686266711E-15, -1.000000000000000000 ) ) ;
#77746=ORIENTED_EDGE ( 'NONE', *, *, #68173, .F. ) ;
#77813=CARTESIAN_POINT ( 'NONE',  ( 13.43663047529820709, 66.55335465531679517, -118.1123010284241985 ) ) ;
#77942=DIRECTION ( 'NONE',  ( -0.000000000000000000, -6.982962677686266711E-15, 1.000000000000000000 ) ) ;
#78016=PLANE ( 'NONE',  #42142 ) ;
#78083=CARTESIAN_POINT ( 'NONE',  ( -16.97683809663752186, 66.15000000001201386, -116.4254715027206828 ) ) ;
#78087=ORIENTED_EDGE ( 'NONE', *, *, #237819, .F. ) ;
#78101=ORIENTED_EDGE ( 'NONE', *, *, #229810, .F. ) ;
#78156=AXIS2_PLACEMENT_3D ( 'NONE', #217754, #176113, #58682 ) ;
#78258=CARTESIAN_POINT ( 'NONE',  ( -16.87372397896796983, 66.11940046337028321, -116.1723829744886558 ) ) ;
#78311=CARTESIAN_POINT ( 'NONE',  ( -16.86379686415369150, 66.02478224075885294, -115.5897175954340810 ) ) ;
#78354=ORIENTED_EDGE ( 'NONE', *, *, #221700, .F. ) ;
#78409=ORIENTED_EDGE ( 'NONE', *, *, #199743, .T. ) ;
#78477=DIRECTION ( 'NONE',  ( -1.000000000000000000, 0.000000000000000000, -0.000000000000000000 ) ) ;
#78480=DIRECTION ( 'NONE',  ( 0.000000000000000000, 1.000000000000000000, 6.982962677686266711E-15 ) ) ;
#78597=VERTEX_POINT ( 'NONE', #221792 ) ;
#78847=CARTESIAN_POINT ( 'NONE',  ( 18.39999999999999503, 70.35000000001201670, -115.6731074845243370 ) ) ;
#79134=DIRECTION ( 'NONE',  ( -1.000000000000000000, -0.000000000000000000, -0.000000000000000000 ) ) ;
#79326=CARTESIAN_POINT ( 'NONE',  ( 18.39999999999999503, 64.25000000001202238, -115.6731074845243938 ) ) ;
#79343=FACE_OUTER_BOUND ( 'NONE', #96937, .T. ) ;
#79398=VERTEX_POINT ( 'NONE', #205148 ) ;
#79584=CARTESIAN_POINT ( 'NONE',  ( -18.40000000000000213, 64.58541674041221370, -115.6731074845243938 ) ) ;
#79626=VERTEX_POINT ( 'NONE', #137186 ) ;
#79801=DIRECTION ( 'NONE',  ( 1.186688945009010077E-16, 1.000000000000000000, 6.982962677686266711E-15 ) ) ;
#79879=VERTEX_POINT ( 'NONE', #66645 ) ;
#80111=ORIENTED_EDGE ( 'NONE', *, *, #13507, .F. ) ;
#80156=CARTESIAN_POINT ( 'NONE',  ( -18.40000000000000213, 70.35000000001207354, -123.8731074845243398 ) ) ;
#80268=CARTESIAN_POINT ( 'NONE',  ( 20.99999999999999645, 66.25000000001202238, -115.6731074845243796 ) ) ;
#80402=CARTESIAN_POINT ( 'NONE',  ( -16.87487986503753845, 66.04999244492645971, -123.8731327448376334 ) ) ;
#81133=EDGE_LOOP ( 'NONE', ( #156375, #184949, #161787, #92227, #192678, #16417, #77746, #95965, #139196, #222645, #69327, #131033, #142498, #9588 ) ) ;
#81303=LINE ( 'NONE', #164736, #132734 ) ;
#81391=CARTESIAN_POINT ( 'NONE',  ( 15.74999999999999645, 66.15000000001204228, -119.7731074845243739 ) ) ;
#81479=DIRECTION ( 'NONE',  ( -0.000000000000000000, -6.982962677686266711E-15, 1.000000000000000000 ) ) ;
#81566=CARTESIAN_POINT ( 'NONE',  ( -17.73285935862681484, 65.14201819622762457, -126.2816692942949857 ) ) ;
#81689=CARTESIAN_POINT ( 'NONE',  ( 16.27683809663749770, 66.65000000001209912, -127.2731074845243597 ) ) ;
#82319=ORIENTED_EDGE ( 'NONE', *, *, #192141, .T. ) ;
#82353=CARTESIAN_POINT ( 'NONE',  ( -16.94445028196807002, 66.00793639031427062, -115.6304376629428106 ) ) ;
#82422=CARTESIAN_POINT ( 'NONE',  ( 20.27550659511088682, 66.78395627750320784, -123.8731074845243683 ) ) ;
#82459=CARTESIAN_POINT ( 'NONE',  ( -18.40000000000000213, 64.52683809664958403, -123.9731074845243768 ) ) ;
#82871=DIRECTION ( 'NONE',  ( 0.000000000000000000, 0.000000000000000000, -1.000000000000000000 ) ) ;
#83049=DIRECTION ( 'NONE',  ( -0.000000000000000000, -6.982962677686266711E-15, 1.000000000000000000 ) ) ;
#83151=DIRECTION ( 'NONE',  ( 1.186688945009010077E-16, 1.000000000000000000, 6.982962677686266711E-15 ) ) ;
#83497=PLANE ( 'NONE',  #165879 ) ;
#83612=FACE_OUTER_BOUND ( 'NONE', #219464, .T. ) ;
#83707=CARTESIAN_POINT ( 'NONE',  ( -18.39999999999999858, 64.25000000001210765, -127.2731074845243882 ) ) ;
#83829=EDGE_CURVE ( 'NONE', #212715, #17807, #149972, .T. ) ;
#83881=( NAMED_UNIT ( * ) SI_UNIT ( $, .STERADIAN. ) SOLID_ANGLE_UNIT ( ) );
#83942=CARTESIAN_POINT ( 'NONE',  ( -16.85722902420155478, 66.05000000001200533, -115.7886549582948845 ) ) ;
#84215=LINE ( 'NONE', #163825, #183725 ) ;
#84450=CIRCLE ( 'NONE', #230244, 1.749999999999998002 ) ;
#84566=ORIENTED_EDGE ( 'NONE', *, *, #155826, .T. ) ;
#85026=CARTESIAN_POINT ( 'NONE',  ( -18.40000000000000213, 64.66825945288690036, -123.8731074845243683 ) ) ;
#85073=AXIS2_PLACEMENT_3D ( 'NONE', #96727, #38091, #199735 ) ;
#85099=ADVANCED_FACE ( 'NONE', ( #152348 ), #234404, .F. ) ;
#85241=CARTESIAN_POINT ( 'NONE',  ( -16.96982749440706328, 66.05000000001201954, -116.1478858933360954 ) ) ;
#85358=SURFACE_STYLE_USAGE ( .BOTH. , #167530 ) ;
#85448=CIRCLE ( 'NONE', #93872, 1.749999999999999778 ) ;
#85807=ORIENTED_EDGE ( 'NONE', *, *, #31126, .F. ) ;
#85833=CARTESIAN_POINT ( 'NONE',  ( -16.92209698673559970, 66.05000000001209060, -123.8124719174716546 ) ) ;
#85941=CARTESIAN_POINT ( 'NONE',  ( -16.80117486205003630, 66.05034273169968628, -115.6742526115988881 ) ) ;
#85963=CIRCLE ( 'NONE', #123415, 1.500000000000001332 ) ;
#86066=ORIENTED_EDGE ( 'NONE', *, *, #36326, .F. ) ;
#86090=CARTESIAN_POINT ( 'NONE',  ( -18.35663730107557257, 64.52609257350087546, -127.2731074845243882 ) ) ;
#86190=PLANE ( 'NONE',  #21186 ) ;
#86222=CARTESIAN_POINT ( 'NONE',  ( -16.88853107394619357, 66.04912151666502496, -115.6701711376321384 ) ) ;
#86226=DIRECTION ( 'NONE',  ( 1.000000000000000000, 0.000000000000000000, 0.000000000000000000 ) ) ;
#86307=CARTESIAN_POINT ( 'NONE',  ( 18.54999999999999716, 52.34166666667870516, -119.7731074845244592 ) ) ;
#86367=VECTOR ( 'NONE', #58540, 999.9999999999998863 ) ;
#86531=CARTESIAN_POINT ( 'NONE',  ( -16.88705144915408951, 66.05000000001200533, -115.9540860792368733 ) ) ;
#86533=LINE ( 'NONE', #81391, #154977 ) ;
#86573=DIRECTION ( 'NONE',  ( 1.000000000000000000, -1.186688945009009831E-16, -8.286604613020806758E-31 ) ) ;
#86666=PRODUCT_DEFINITION ( 'UNKNOWN', '', #182049, #3538 ) ;
#86699=( BOUNDED_CURVE ( )  B_SPLINE_CURVE ( 3, ( #61442, #200948, #144808, #159275 ),
 .UNSPECIFIED., .F., .F. ) 
 B_SPLINE_CURVE_WITH_KNOTS ( ( 4, 4 ),
 ( 2.589852378279005496, 2.850972632318389710 ),
 .UNSPECIFIED. ) 
 CURVE ( )  GEOMETRIC_REPRESENTATION_ITEM ( )  RATIONAL_B_SPLINE_CURVE ( ( 1.000000000000000000, 0.9943260843901261525, 0.9943260843901261525, 1.000000000000000000 ) ) 
 REPRESENTATION_ITEM ( '' )  );
#86827=EDGE_CURVE ( 'NONE', #18395, #184009, #255375, .T. ) ;
#87026=DIRECTION ( 'NONE',  ( 1.000000000000000000, 0.000000000000000000, 0.000000000000000000 ) ) ;
#87449=DIRECTION ( 'NONE',  ( -1.000000000000000000, 0.000000000000000000, 0.000000000000000000 ) ) ;
#87547=CARTESIAN_POINT ( 'NONE',  ( -16.97683809663752186, 66.05000000001207638, -123.1207434663278804 ) ) ;
#87606=EDGE_CURVE ( 'NONE', #105369, #5646, #51762, .T. ) ;
#87810=CARTESIAN_POINT ( 'NONE',  ( -16.87998658237755834, 66.05000000001207638, -123.6594679167868236 ) ) ;
#87820=CARTESIAN_POINT ( 'NONE',  ( -16.80070461187894892, 66.05000000001203375, -115.6700713136833798 ) ) ;
#87830=AXIS2_PLACEMENT_3D ( 'NONE', #63398, #240777, #5988 ) ;
#87843=CARTESIAN_POINT ( 'NONE',  ( 20.27550659511089037, 66.78395627750315100, -115.6731074845243654 ) ) ;
#87855=CARTESIAN_POINT ( 'NONE',  ( -16.94389599338511943, 66.00880201025701410, -123.9154626827141215 ) ) ;
#87869=CARTESIAN_POINT ( 'NONE',  ( -13.88555196119804158, 66.54256847116315043, -121.5231905466247753 ) ) ;
#87966=AXIS2_PLACEMENT_3D ( 'NONE', #9221, #168352, #150044 ) ;
#87982=ORIENTED_EDGE ( 'NONE', *, *, #40436, .F. ) ;
#88000=VECTOR ( 'NONE', #25994, 1000.000000000000000 ) ;
#88611=DIRECTION ( 'NONE',  ( 0.000000000000000000, -1.000000000000000000, -6.982962677686266711E-15 ) ) ;
#89118=CARTESIAN_POINT ( 'NONE',  ( -16.87683809663750623, 66.05000000001206217, -123.1207434663278946 ) ) ;
#89146=DIRECTION ( 'NONE',  ( 0.7071067811865493491, -0.7071067811865456854, -4.937700262164518065E-15 ) ) ;
#89285=CYLINDRICAL_SURFACE ( 'NONE', #47399, 1.500000000000001332 ) ;
#89492=PLANE ( 'NONE',  #75196 ) ;
#89667=ORIENTED_EDGE ( 'NONE', *, *, #160740, .T. ) ;
#89675=FACE_OUTER_BOUND ( 'NONE', #17224, .T. ) ;
#90086=CARTESIAN_POINT ( 'NONE',  ( -17.11825945287482753, 65.95000000001208207, -123.8731074845243683 ) ) ;
#90162=CARTESIAN_POINT ( 'NONE',  ( -18.40000000000000213, 64.25000000001207923, -123.8731074845243683 ) ) ;
#90256=ORIENTED_EDGE ( 'NONE', *, *, #41132, .F. ) ;
#90266=B_SPLINE_CURVE_WITH_KNOTS ( 'NONE', 3,
 ( #127832, #207374, #110817, #86090, #9160, #49570, #190386 ),
 .UNSPECIFIED., .F., .F.,
 ( 4, 3, 4 ),
 ( 0.000000000000000000, 4.520325912680430423E-05, 5.794988040901246848E-05 ),
 .UNSPECIFIED. ) ;
#90302=EDGE_CURVE ( 'NONE', #7208, #64566, #205570, .T. ) ;
#90358=CARTESIAN_POINT ( 'NONE',  ( 15.39793903038207823, 66.61031399435637468, -120.8502639781730750 ) ) ;
#90396=CARTESIAN_POINT ( 'NONE',  ( -16.82542659449982736, 66.06550010858471467, -123.7784718844978897 ) ) ;
#90475=ORIENTED_EDGE ( 'NONE', *, *, #6008, .T. ) ;
#90655=CARTESIAN_POINT ( 'NONE',  ( 21.72449340488910252, 65.71604372252093640, -123.8731074845243683 ) ) ;
#90843=CARTESIAN_POINT ( 'NONE',  ( -16.89318236219977010, 66.04846474213692886, -123.8782371166302312 ) ) ;
#90901=ORIENTED_EDGE ( 'NONE', *, *, #110300, .F. ) ;
#90904=VERTEX_POINT ( 'NONE', #58059 ) ;
#90959=VECTOR ( 'NONE', #54839, 1000.000000000000000 ) ;
#90979=DIRECTION ( 'NONE',  ( 1.000000000000000000, -7.125593699324843413E-30, 1.020425574104004196E-15 ) ) ;
#91383=CARTESIAN_POINT ( 'NONE',  ( -18.37013991200266005, 64.50025238380001724, -112.2300844740072705 ) ) ;
#91425=LINE ( 'NONE', #172289, #90959 ) ;
#91591=CARTESIAN_POINT ( 'NONE',  ( -20.65000000000000568, 68.75000000001209344, -127.2731074845243597 ) ) ;
#91603=CARTESIAN_POINT ( 'NONE',  ( 20.73486653747088937, 68.25000000001205080, -127.2731074845243597 ) ) ;
#91691=CARTESIAN_POINT ( 'NONE',  ( -16.77431908686106610, 66.05419424549407381, -123.8589467021746060 ) ) ;
#91753=CARTESIAN_POINT ( 'NONE',  ( -12.84409460144753723, 66.58931770574410791, -121.0919640425761088 ) ) ;
#91820=ORIENTED_EDGE ( 'NONE', *, *, #155403, .F. ) ;
#92227=ORIENTED_EDGE ( 'NONE', *, *, #110518, .T. ) ;
#92359=ORIENTED_EDGE ( 'NONE', *, *, #156478, .F. ) ;
#92387=ORIENTED_EDGE ( 'NONE', *, *, #156478, .T. ) ;
#92528=CARTESIAN_POINT ( 'NONE',  ( -21.65000000000000213, 66.05000000001201954, -115.7731074845243597 ) ) ;
#92846=EDGE_CURVE ( 'NONE', #41514, #176240, #241087, .T. ) ;
#93004=CARTESIAN_POINT ( 'NONE',  ( -16.90987985657661241, 66.04219248183227364, -115.6538203956407358 ) ) ;
#93147=VECTOR ( 'NONE', #118036, 1000.000000000000000 ) ;
#93150=DIRECTION ( 'NONE',  ( -0.000000000000000000, -6.982962677686266711E-15, 1.000000000000000000 ) ) ;
#93208=( BOUNDED_CURVE ( )  B_SPLINE_CURVE ( 3, ( #163260, #6735, #23766, #164542 ),
 .UNSPECIFIED., .F., .F. ) 
 B_SPLINE_CURVE_WITH_KNOTS ( ( 4, 4 ),
 ( 1.570796326794908992, 2.617993877991481533 ),
 .UNSPECIFIED. ) 
 CURVE ( )  GEOMETRIC_REPRESENTATION_ITEM ( )  RATIONAL_B_SPLINE_CURVE ( ( 1.000000000000000000, 0.9106836025229633202, 0.9106836025229633202, 1.000000000000000000 ) ) 
 REPRESENTATION_ITEM ( '' )  );
#93386=CARTESIAN_POINT ( 'NONE',  ( -12.68215100488890101, 66.60336962369433422, -118.6160500917060858 ) ) ;
#93395=EDGE_CURVE ( 'NONE', #19871, #51212, #146753, .T. ) ;
#93451=DIRECTION ( 'NONE',  ( 0.000000000000000000, -1.000000000000000000, -6.982962677686266711E-15 ) ) ;
#93506=DIRECTION ( 'NONE',  ( -0.000000000000000000, -6.982962677686266711E-15, 1.000000000000000000 ) ) ;
#93536=CARTESIAN_POINT ( 'NONE',  ( 13.12229106158773639, 66.56936289831530473, -118.2548468664634385 ) ) ;
#93594=CARTESIAN_POINT ( 'NONE',  ( -16.93906926870270624, 65.98785312906551326, -123.9696551772975539 ) ) ;
#93617=CARTESIAN_POINT ( 'NONE',  ( -23.25000000000000355, 70.35000000001201670, -115.6731074845243370 ) ) ;
#93771=ORIENTED_EDGE ( 'NONE', *, *, #117380, .T. ) ;
#93872=AXIS2_PLACEMENT_3D ( 'NONE', #108394, #250459, #86226 ) ;
#94024=CARTESIAN_POINT ( 'NONE',  ( -16.87786941232800686, 66.04184528586702640, -115.6459216847303537 ) ) ;
#94130=CARTESIAN_POINT ( 'NONE',  ( 22.88900146558018989, 67.29609520889924568, -123.8731074845243683 ) ) ;
#94201=FACE_BOUND ( 'NONE', #254676, .T. ) ;
#94281=CARTESIAN_POINT ( 'NONE',  ( -16.92563707711778775, 66.03100930561521409, -115.6423491850004126 ) ) ;
#94366=VERTEX_POINT ( 'NONE', #216416 ) ;
#94485=ORIENTED_EDGE ( 'NONE', *, *, #234019, .T. ) ;
#94669=CARTESIAN_POINT ( 'NONE',  ( -12.48127053791144903, 66.62341902196808974, -118.8961612375124446 ) ) ;
#94819=CARTESIAN_POINT ( 'NONE',  ( 15.74999999999999645, 66.65000000001204228, -119.7731074845243739 ) ) ;
#94836=ORIENTED_EDGE ( 'NONE', *, *, #56662, .F. ) ;
#94984=EDGE_LOOP ( 'NONE', ( #110227, #17090, #87982, #26162 ) ) ;
#95101=EDGE_CURVE ( 'NONE', #30385, #176240, #117668, .T. ) ;
#95565=CARTESIAN_POINT ( 'NONE',  ( 16.87683809663750267, 66.05000000001207638, -123.8731074845243683 ) ) ;
#95586=CARTESIAN_POINT ( 'NONE',  ( -16.90202395485833264, 66.03405545546138455, -115.6200937632638954 ) ) ;
#95709=AXIS2_PLACEMENT_3D ( 'NONE', #108994, #169027, #69910 ) ;
#95849=PLANE ( 'NONE',  #209193 ) ;
#95929=CARTESIAN_POINT ( 'NONE',  ( -16.86133551771148475, 66.05000000001201954, -115.7217640499777360 ) ) ;
#95965=ORIENTED_EDGE ( 'NONE', *, *, #57099, .F. ) ;
#95997=CARTESIAN_POINT ( 'NONE',  ( -16.89268316805466341, 66.04827818676987761, -123.8788599630699281 ) ) ;
#96090=CARTESIAN_POINT ( 'NONE',  ( 13.22461703343585526, 66.56333706821293106, -118.2000707522294647 ) ) ;
#96524=FACE_OUTER_BOUND ( 'NONE', #48850, .T. ) ;
#96568=ORIENTED_EDGE ( 'NONE', *, *, #140713, .T. ) ;
#96727=CARTESIAN_POINT ( 'NONE',  ( 13.99999999999999822, 66.15000000001204228, -119.7731074845243739 ) ) ;
#96756=ORIENTED_EDGE ( 'NONE', *, *, #170683, .T. ) ;
#96931=LINE ( 'NONE', #176526, #218812 ) ;
#96937=EDGE_LOOP ( 'NONE', ( #183050, #73457, #168778, #36404, #65432 ) ) ;
#97091=DIRECTION ( 'NONE',  ( -1.020425574104004196E-15, 6.982962677686266711E-15, -1.000000000000000000 ) ) ;
#97195=CARTESIAN_POINT ( 'NONE',  ( -15.06720934482788365, 66.58230930894893618, -118.3815067877597897 ) ) ;
#97397=ORIENTED_EDGE ( 'NONE', *, *, #118195, .T. ) ;
#97592=DIRECTION ( 'NONE',  ( 1.000000000000000000, 7.492892343619937423E-30, -1.073024830501117725E-15 ) ) ;
#97804=CARTESIAN_POINT ( 'NONE',  ( -16.81744102076748959, 66.05000000001201954, -115.6731074845243796 ) ) ;
#97814=CARTESIAN_POINT ( 'NONE',  ( -21.65000000000000213, 68.75000000001209344, -127.2731074845243597 ) ) ;
#97928=DIRECTION ( 'NONE',  ( 1.000000000000000000, -1.186688945009010077E-16, -8.286604613020808509E-31 ) ) ;
#98026=FACE_OUTER_BOUND ( 'NONE', #119674, .T. ) ;
#98062=CARTESIAN_POINT ( 'NONE',  ( -17.04761207306817283, 65.97354912661423043, -115.6731074845243938 ) ) ;
#98070=DIRECTION ( 'NONE',  ( -0.7071067811865463515, 0.7071067811865487940, 4.178957128135655137E-15 ) ) ;
#98075=ORIENTED_EDGE ( 'NONE', *, *, #188336, .F. ) ;
#98167=ORIENTED_EDGE ( 'NONE', *, *, #228944, .F. ) ;
#98192=VERTEX_POINT ( 'NONE', #166650 ) ;
#98288=DIRECTION ( 'NONE',  ( 1.000000000000000000, -0.000000000000000000, 0.000000000000000000 ) ) ;
#98303=ORIENTED_EDGE ( 'NONE', *, *, #166863, .F. ) ;
#98419=MECHANICAL_DESIGN_GEOMETRIC_PRESENTATION_REPRESENTATION('',(#148165),#248309);
#98422=ADVANCED_FACE ( 'NONE', ( #162467 ), #199011, .T. ) ;
#98477=CARTESIAN_POINT ( 'NONE',  ( -15.66061380678752535, 66.63927620602598267, -119.2091802899176685 ) ) ;
#98631=CARTESIAN_POINT ( 'NONE',  ( 15.73863059295127798, 66.64859682587035650, -119.5435770476858863 ) ) ;
#98938=CARTESIAN_POINT ( 'NONE',  ( 21.72449340488910252, 65.71604372252093640, -123.8731074845243683 ) ) ;
#98974=CARTESIAN_POINT ( 'NONE',  ( -18.40000000000000213, 64.52683809665002457, -112.3229367329901152 ) ) ;
#99092=CARTESIAN_POINT ( 'NONE',  ( -16.87683809663752399, 66.13508655273184900, -116.2988259332204564 ) ) ;
#99147=CARTESIAN_POINT ( 'NONE',  ( -18.40000000000000213, 64.52683809664954140, -115.6316861282870860 ) ) ;
#99477=ORIENTED_EDGE ( 'NONE', *, *, #36456, .T. ) ;
#99496=CARTESIAN_POINT ( 'NONE',  ( -18.34374000495059676, 64.52683809664949877, -112.2731074845243739 ) ) ;
#99811=ORIENTED_EDGE ( 'NONE', *, *, #111124, .T. ) ;
#99848=CARTESIAN_POINT ( 'NONE',  ( -16.94107738177415357, 65.98576071487543970, -123.9731074845243768 ) ) ;
#99870=ORIENTED_EDGE ( 'NONE', *, *, #126211, .T. ) ;
#99973=CARTESIAN_POINT ( 'NONE',  ( -16.89268316805466341, 66.04827818676987761, -123.8788599630699281 ) ) ;
#100192=DIRECTION ( 'NONE',  ( -0.000000000000000000, -6.982962677686266711E-15, 1.000000000000000000 ) ) ;
#100556=DIRECTION ( 'NONE',  ( 1.186688945009009831E-16, 1.000000000000000000, 6.982962677686266711E-15 ) ) ;
#100741=ORIENTED_EDGE ( 'NONE', *, *, #51974, .F. ) ;
#100923=LINE ( 'NONE', #16327, #50327 ) ;
#101005=ORIENTED_EDGE ( 'NONE', *, *, #24452, .F. ) ;
#101187=CIRCLE ( 'NONE', #42990, 0.5000000000000004441 ) ;
#101201=ORIENTED_EDGE ( 'NONE', *, *, #118024, .F. ) ;
#101439=DIRECTION ( 'NONE',  ( -0.7071067811865301422, 0.7071067811865648922, 0.000000000000000000 ) ) ;
#101469=VECTOR ( 'NONE', #186314, 1000.000000000000000 ) ;
#101544=CARTESIAN_POINT ( 'NONE',  ( -17.11825945287482753, 66.05000000001207638, -123.8731074845243683 ) ) ;
#101846=ORIENTED_EDGE ( 'NONE', *, *, #243929, .F. ) ;
#101884=VECTOR ( 'NONE', #210473, 1000.000000000000000 ) ;
#101944=VECTOR ( 'NONE', #156081, 1000.000000000000000 ) ;
#102008=DIRECTION ( 'NONE',  ( 1.073024830501117725E-15, 6.982962677686266711E-15, -1.000000000000000000 ) ) ;
#102124=EDGE_LOOP ( 'NONE', ( #145653, #155268, #128460, #217084 ) ) ;
#102172=SURFACE_STYLE_USAGE ( .BOTH. , #141335 ) ;
#102183=VECTOR ( 'NONE', #195001, 1000.000000000000000 ) ;
#102356=ORIENTED_EDGE ( 'NONE', *, *, #245029, .F. ) ;
#102398=CARTESIAN_POINT ( 'NONE',  ( -16.87845715379269507, 66.04214188611504710, -123.8993068334654737 ) ) ;
#102556=VECTOR ( 'NONE', #131530, 1000.000000000000000 ) ;
#102835=CARTESIAN_POINT ( 'NONE',  ( -18.40000000000000213, 64.52132590001208712, -112.2978007008649826 ) ) ;
#103013=LINE ( 'NONE', #180018, #201653 ) ;
#103150=CARTESIAN_POINT ( 'NONE',  ( 21.72449340488910607, 65.71604372252096482, -127.2731074845243597 ) ) ;
#103347=ORIENTED_EDGE ( 'NONE', *, *, #121235, .T. ) ;
#103386=EDGE_LOOP ( 'NONE', ( #45964, #146704, #176463, #103444 ) ) ;
#103444=ORIENTED_EDGE ( 'NONE', *, *, #148271, .T. ) ;
#103538=CARTESIAN_POINT ( 'NONE',  ( -16.87683809663752399, 66.13411015068005838, -116.2905342915937581 ) ) ;
#103642=AXIS2_PLACEMENT_3D ( 'NONE', #123778, #27277, #125066 ) ;
#103647=LINE ( 'NONE', #42415, #2664 ) ;
#103705=CARTESIAN_POINT ( 'NONE',  ( -18.41431012584568450, 64.51252797080390167, -127.2963434976260686 ) ) ;
#103913=AXIS2_PLACEMENT_3D ( 'NONE', #165198, #83049, #107786 ) ;
#103952=DIRECTION ( 'NONE',  ( -1.000000000000000000, -7.125593699324843413E-30, 1.020425574104004196E-15 ) ) ;
#104042=ORIENTED_EDGE ( 'NONE', *, *, #56662, .T. ) ;
#104120=EDGE_LOOP ( 'NONE', ( #66950, #207069, #51664, #121402 ) ) ;
#104126=CARTESIAN_POINT ( 'NONE',  ( -17.11825945287482753, 65.95000000001208207, -123.8731074845243683 ) ) ;
#104429=CARTESIAN_POINT ( 'NONE',  ( -16.87683809663752399, 66.15000000001205649, -123.1207434663280651 ) ) ;
#104472=PLANE ( 'NONE',  #176446 ) ;
#104553=LINE ( 'NONE', #82422, #113255 ) ;
#104589=CARTESIAN_POINT ( 'NONE',  ( -18.40000000000000213, 64.52683809664959824, -123.9145288407616903 ) ) ;
#105044=CARTESIAN_POINT ( 'NONE',  ( -33.72168855820452649, 64.52683809664961245, -127.2731074845243882 ) ) ;
#105280=CARTESIAN_POINT ( 'NONE',  ( 20.73486653747088937, 68.25000000001197975, -115.6731074845243654 ) ) ;
#105320=CARTESIAN_POINT ( 'NONE',  ( -18.40000000000000213, 70.35000000001201670, -115.6731074845243370 ) ) ;
#105369=VERTEX_POINT ( 'NONE', #169545 ) ;
#105391=CARTESIAN_POINT ( 'NONE',  ( -16.95709691156408283, 66.05000000001209060, -123.8630499220137864 ) ) ;
#105400=EDGE_CURVE ( 'NONE', #66849, #212706, #15250, .T. ) ;
#105440=PRODUCT_DEFINITION_SHAPE ( 'NONE', 'NONE',  #86666 ) ;
#105500=CARTESIAN_POINT ( 'NONE',  ( -16.79363873026997922, 66.05114977059356818, -115.6769537030788939 ) ) ;
#105613=DIRECTION ( 'NONE',  ( -1.020425574104004196E-15, -6.982962677686266711E-15, 1.000000000000000000 ) ) ;
#105836=ORIENTED_EDGE ( 'NONE', *, *, #172165, .F. ) ;
#106047=ORIENTED_EDGE ( 'NONE', *, *, #205441, .T. ) ;
#106057=CARTESIAN_POINT ( 'NONE',  ( 23.24999999999999645, 64.25000000001202238, -115.6731074845243938 ) ) ;
#106087=CARTESIAN_POINT ( 'NONE',  ( -16.92280123533699410, 66.05000000001207638, -123.6724751704392702 ) ) ;
#106098=CARTESIAN_POINT ( 'NONE',  ( -16.97683810757273193, 66.05000000001201954, -116.2866841969848082 ) ) ;
#106101=DIRECTION ( 'NONE',  ( -1.000000000000000000, -1.652117596168391700E-15, -1.153667551319263085E-29 ) ) ;
#106147=FACE_OUTER_BOUND ( 'NONE', #55712, .T. ) ;
#106165=ORIENTED_EDGE ( 'NONE', *, *, #216935, .F. ) ;
#106354=LINE ( 'NONE', #226300, #145550 ) ;
#106365=AXIS2_PLACEMENT_3D ( 'NONE', #195244, #156120, #174421 ) ;
#106529=ORIENTED_EDGE ( 'NONE', *, *, #31126, .T. ) ;
#107087=VECTOR ( 'NONE', #181999, 1000.000000000000000 ) ;
#107095=ORIENTED_EDGE ( 'NONE', *, *, #132674, .F. ) ;
#107161=ORIENTED_EDGE ( 'NONE', *, *, #248566, .T. ) ;
#107243=VERTEX_POINT ( 'NONE', #4083 ) ;
#107281=VECTOR ( 'NONE', #206762, 1000.000000000000000 ) ;
#107392=CARTESIAN_POINT ( 'NONE',  ( -16.84793658983414488, 66.05000000001231797, -123.7894608067136346 ) ) ;
#107449=CARTESIAN_POINT ( 'NONE',  ( 21.72449340488910252, 65.71604372252096482, -127.2731074845243597 ) ) ;
#107460=CARTESIAN_POINT ( 'NONE',  ( -12.47155713865592119, 66.62433047358626936, -120.6553174751384176 ) ) ;
#107508=DIRECTION ( 'NONE',  ( -0.5932847527679310229, -0.8049926720990042694, -4.984624513800578906E-15 ) ) ;
#107786=DIRECTION ( 'NONE',  ( -1.000000000000000000, 0.000000000000000000, 0.000000000000000000 ) ) ;
#107992=VECTOR ( 'NONE', #158442, 1000.000000000000000 ) ;
#108379=CARTESIAN_POINT ( 'NONE',  ( -16.91256925476570672, 66.01426884188381905, -115.5554649955190882 ) ) ;
#108394=CARTESIAN_POINT ( 'NONE',  ( -14.00000000000000178, 66.15000000001204228, -119.7731074845243739 ) ) ;
#108420=CARTESIAN_POINT ( 'NONE',  ( -16.90137573187934095, 66.05000000001210481, -123.7346900604274964 ) ) ;
#108653=ADVANCED_FACE ( 'NONE', ( #119888 ), #193373, .T. ) ;
#108680=AXIS2_PLACEMENT_3D ( 'NONE', #48460, #184116, #144983 ) ;
#108707=ORIENTED_EDGE ( 'NONE', *, *, #158958, .T. ) ;
#108737=CARTESIAN_POINT ( 'NONE',  ( 13.99999999999999822, 66.15000000001204228, -119.7731074845243739 ) ) ;
#108771=CYLINDRICAL_SURFACE ( 'NONE', #3092, 0.1000000000000028644 ) ;
#108773=ORIENTED_EDGE ( 'NONE', *, *, #240960, .F. ) ;
#108854=CARTESIAN_POINT ( 'NONE',  ( 20.04999999999999716, 67.25000000001206502, -127.2731074845243597 ) ) ;
#108994=CARTESIAN_POINT ( 'NONE',  ( 20.99999999999999645, 66.25000000001202238, -115.6731074845243796 ) ) ;
#109153=ORIENTED_EDGE ( 'NONE', *, *, #169118, .T. ) ;
#109173=CARTESIAN_POINT ( 'NONE',  ( 20.05000000000002913, 68.75000000001203659, -123.8731074845243540 ) ) ;
#109222=VERTEX_POINT ( 'NONE', #9867 ) ;
#109310=ORIENTED_EDGE ( 'NONE', *, *, #172636, .T. ) ;
#109327=CARTESIAN_POINT ( 'NONE',  ( -18.40000000000000213, 64.52683809664949877, -112.2731074845243739 ) ) ;
#109411=CARTESIAN_POINT ( 'NONE',  ( -14.00000000000000178, 66.15000000001204228, -119.7731074845243739 ) ) ;
#109429=FACE_OUTER_BOUND ( 'NONE', #81133, .T. ) ;
#109531=CARTESIAN_POINT ( 'NONE',  ( -16.94107738177414291, 65.98576071487538286, -115.5731074845243711 ) ) ;
#109632=CARTESIAN_POINT ( 'NONE',  ( -18.40000000000000213, 70.35000000001201670, -115.6731074845243370 ) ) ;
#109640=CARTESIAN_POINT ( 'NONE',  ( -18.41431012584569515, 64.51252797080381640, -112.2498714714227219 ) ) ;
#109730=ORIENTED_EDGE ( 'NONE', *, *, #39055, .F. ) ;
#109847=ORIENTED_EDGE ( 'NONE', *, *, #40766, .T. ) ;
#109982=DIRECTION ( 'NONE',  ( 1.000000000000000000, 0.000000000000000000, 0.000000000000000000 ) ) ;
#110090=FILL_AREA_STYLE ('',( #68406 ) ) ;
#110227=ORIENTED_EDGE ( 'NONE', *, *, #15779, .T. ) ;
#110229=VECTOR ( 'NONE', #12850, 1000.000000000000000 ) ;
#110300=EDGE_CURVE ( 'NONE', #144523, #166838, #70425, .T. ) ;
#110518=EDGE_CURVE ( 'NONE', #124526, #7935, #177988, .T. ) ;
#110596=DIRECTION ( 'NONE',  ( -0.7071067811865463515, -0.7071067811865487940, -4.937700262164540154E-15 ) ) ;
#110728=DIRECTION ( 'NONE',  ( 1.000000000000000000, 7.492892343619937423E-30, -1.073024830501117725E-15 ) ) ;
#110817=CARTESIAN_POINT ( 'NONE',  ( -18.37160782347004329, 64.52438358520969075, -127.2731074845243882 ) ) ;
#110936=CARTESIAN_POINT ( 'NONE',  ( -16.87036670365548474, 66.01058118071034642, -115.5435473672223168 ) ) ;
#111124=EDGE_CURVE ( 'NONE', #51212, #176240, #86699, .T. ) ;
#111901=ORIENTED_EDGE ( 'NONE', *, *, #68173, .T. ) ;
#111904=DIRECTION ( 'NONE',  ( -1.000000000000000000, 1.646408749285562691E-14, 1.149681084847720908E-28 ) ) ;
#111984=CARTESIAN_POINT ( 'NONE',  ( -15.75000000000000355, 66.15000000001204228, -119.7731074845243739 ) ) ;
#112173=ORIENTED_EDGE ( 'NONE', *, *, #5820, .F. ) ;
#112320=CARTESIAN_POINT ( 'NONE',  ( -21.64999999999999858, 66.65000000001201386, -115.6731074845243654 ) ) ;
#112364=ORIENTED_EDGE ( 'NONE', *, *, #114650, .F. ) ;
#112653=LINE ( 'NONE', #190930, #101884 ) ;
#112864=CARTESIAN_POINT ( 'NONE',  ( -17.11825945287481687, 66.05000000001201954, -115.7731074845243739 ) ) ;
#112952=CARTESIAN_POINT ( 'NONE',  ( -16.94226253665225457, 66.05000000001200533, -115.9698420801400971 ) ) ;
#113023=EDGE_CURVE ( 'NONE', #3872, #41514, #84215, .T. ) ;
#113157=CARTESIAN_POINT ( 'NONE',  ( -16.93772744219066340, 66.00645889125971166, -123.9250455125546750 ) ) ;
#113255=VECTOR ( 'NONE', #227091, 1000.000000000000000 ) ;
#113377=DIRECTION ( 'NONE',  ( -1.000000000000000000, 0.000000000000000000, 0.000000000000000000 ) ) ;
#113841=CARTESIAN_POINT ( 'NONE',  ( 20.73486653747088582, 68.75000000001203659, -123.8731074845243540 ) ) ;
#113894=STYLED_ITEM ( 'NONE', ( #147944 ), #25248 ) ;
#113956=AXIS2_PLACEMENT_3D ( 'NONE', #219874, #201592, #242005 ) ;
#114052=ORIENTED_EDGE ( 'NONE', *, *, #128157, .T. ) ;
#114199=CARTESIAN_POINT ( 'NONE',  ( -12.25000000000000178, 66.65000000001204228, -119.7731074845243739 ) ) ;
#114227=CARTESIAN_POINT ( 'NONE',  ( -18.40000000000000213, 64.52683809664951298, -115.5731074845243853 ) ) ;
#114335=ADVANCED_FACE ( 'NONE', ( #33372 ), #95849, .F. ) ;
#114392=CARTESIAN_POINT ( 'NONE',  ( 12.30626653967340722, 66.64320997496615462, -119.3182809759104828 ) ) ;
#114430=AXIS2_PLACEMENT_3D ( 'NONE', #63642, #222700, #205713 ) ;
#114470=CARTESIAN_POINT ( 'NONE',  ( 16.27683809663750125, 66.65000000001209912, -127.2731074845243597 ) ) ;
#114635=EDGE_LOOP ( 'NONE', ( #14853, #227191 ) ) ;
#114650=EDGE_CURVE ( 'NONE', #162266, #44866, #176479, .T. ) ;
#114831=CARTESIAN_POINT ( 'NONE',  ( -16.79140778683509794, 66.05505840115743865, -115.6933702507535742 ) ) ;
#114862=COLOUR_RGB ( '', 0.31764706, 0.68627451, 0.89019608) ;
#114962=AXIS2_PLACEMENT_3D ( 'NONE', #123611, #83151, #162750 ) ;
#115034=CARTESIAN_POINT ( 'NONE',  ( -16.81453046979148880, 66.06089771857114101, -123.8113809609213689 ) ) ;
#115287=PLANE ( 'NONE',  #49534 ) ;
#115516=CARTESIAN_POINT ( 'NONE',  ( -12.33960340485503693, 66.63925083009691264, -119.2085373439170866 ) ) ;
#115726=CARTESIAN_POINT ( 'NONE',  ( -16.93440969289731157, 66.00481482419810675, -123.9318732995135832 ) ) ;
#115909=ORIENTED_EDGE ( 'NONE', *, *, #90302, .F. ) ;
#116360=CARTESIAN_POINT ( 'NONE',  ( -33.72168855820452649, 52.34166666667870516, -119.7731074845244592 ) ) ;
#116637=ADVANCED_FACE ( 'NONE', ( #207981 ), #89285, .T. ) ;
#117009=CARTESIAN_POINT ( 'NONE',  ( -16.93339986808596365, 65.99489607144613501, -123.9571138127115120 ) ) ;
#117041=ORIENTED_EDGE ( 'NONE', *, *, #248566, .F. ) ;
#117380=EDGE_CURVE ( 'NONE', #3872, #155298, #121106, .T. ) ;
#117545=CARTESIAN_POINT ( 'NONE',  ( 23.24999999999999645, 64.25000000001210765, -127.2731074845243882 ) ) ;
#117631=CARTESIAN_POINT ( 'NONE',  ( -16.77683809663752257, 52.34166666667870516, -119.7731074845244592 ) ) ;
#117668=LINE ( 'NONE', #18579, #74172 ) ;
#118024=EDGE_CURVE ( 'NONE', #135417, #127391, #23825, .T. ) ;
#118036=DIRECTION ( 'NONE',  ( -1.000000000000000000, 0.000000000000000000, -0.000000000000000000 ) ) ;
#118076=B_SPLINE_CURVE_WITH_KNOTS ( 'NONE', 3,
 ( #219052, #99092, #78258, #39174, #174861, #156563, #134373, #37888, #1285, #254321, #19596, #114831, #18298, #238635 ),
 .UNSPECIFIED., .F., .F.,
 ( 4, 2, 2, 2, 2, 2, 4 ),
 ( 1.387778780781445676E-17, 0.0003823333598418262582, 0.0005735000397627122281, 0.0006690833797231313064, 0.0007168750497033422008, 0.0007407708846934429317, 0.0007646667196835435542 ),
 .UNSPECIFIED. ) ;
#118195=EDGE_CURVE ( 'NONE', #159618, #152369, #10655, .T. ) ;
#118203=LINE ( 'NONE', #214728, #101944 ) ;
#118298=CARTESIAN_POINT ( 'NONE',  ( -16.87435696428308063, 66.04999753707983245, -123.8731157193577985 ) ) ;
#118467=CARTESIAN_POINT ( 'NONE',  ( 20.09999999999999787, 66.25000000001205080, -123.8731074845243683 ) ) ;
#118826=CARTESIAN_POINT ( 'NONE',  ( 20.73486653747088582, 68.75000000001196554, -115.6731074845243512 ) ) ;
#119215=SURFACE_STYLE_FILL_AREA ( #4379 ) ;
#119245=CARTESIAN_POINT ( 'NONE',  ( -16.93826681692523195, 65.98857127972429737, -115.5776490171649300 ) ) ;
#119280=VERTEX_POINT ( 'NONE', #74340 ) ;
#119543=CARTESIAN_POINT ( 'NONE',  ( 14.45963434102924339, 66.54845833862650295, -118.0692319856937900 ) ) ;
#119646=ADVANCED_FACE ( 'NONE', ( #11466 ), #67571, .F. ) ;
#119674=EDGE_LOOP ( 'NONE', ( #183831, #237960, #16485, #220451 ) ) ;
#119811=CARTESIAN_POINT ( 'NONE',  ( 18.54999999999999716, 67.25000000001205080, -127.2731074845243597 ) ) ;
#119888=FACE_OUTER_BOUND ( 'NONE', #136933, .T. ) ;
#119926=ADVANCED_BREP_SHAPE_REPRESENTATION ( '', ( #25248, #2425 ), #227278 ) ;
#120068=ORIENTED_EDGE ( 'NONE', *, *, #142620, .T. ) ;
#120137=ORIENTED_EDGE ( 'NONE', *, *, #114650, .T. ) ;
#120444=ORIENTED_EDGE ( 'NONE', *, *, #148042, .F. ) ;
#120483=AXIS2_PLACEMENT_3D ( 'NONE', #12505, #172887, #52876 ) ;
#120488=LINE ( 'NONE', #3055, #253452 ) ;
#120520=PRESENTATION_STYLE_ASSIGNMENT (( #102172 ) ) ;
#120700=VERTEX_POINT ( 'NONE', #170624 ) ;
#120748=CARTESIAN_POINT ( 'NONE',  ( -16.87368910959167678, 66.03872618332066224, -123.9106143878837827 ) ) ;
#120799=EDGE_CURVE ( 'NONE', #33205, #181057, #56029, .T. ) ;
#120957=UNCERTAINTY_MEASURE_WITH_UNIT (LENGTH_MEASURE( 1.000000000000000082E-05 ), #180467, 'distance_accuracy_value', 'NONE');
#121106=LINE ( 'NONE', #119811, #164324 ) ;
#121235=EDGE_CURVE ( 'NONE', #143067, #135417, #54147, .T. ) ;
#121347=CARTESIAN_POINT ( 'NONE',  ( -16.86337532320260735, 66.02003279578765671, -115.5741830155415499 ) ) ;
#121402=ORIENTED_EDGE ( 'NONE', *, *, #249609, .F. ) ;
#121634=CARTESIAN_POINT ( 'NONE',  ( -23.25000000000000355, 64.25000000001210765, -127.2731074845243882 ) ) ;
#122030=DIRECTION ( 'NONE',  ( 0.2834754621636439431, 0.2834754621636471628, 0.9161240771326858434 ) ) ;
#122128=ORIENTED_EDGE ( 'NONE', *, *, #172636, .F. ) ;
#122421=AXIS2_PLACEMENT_3D ( 'NONE', #105320, #184896, #32272 ) ;
#123381=CARTESIAN_POINT ( 'NONE',  ( 12.25000000000000000, 66.65000000001204228, -119.7731074845243739 ) ) ;
#123413=DIRECTION ( 'NONE',  ( 0.000000000000000000, 1.000000000000000000, 6.982962677686266711E-15 ) ) ;
#123415=AXIS2_PLACEMENT_3D ( 'NONE', #234244, #77729, #176876 ) ;
#123611=CARTESIAN_POINT ( 'NONE',  ( 13.99999999999999822, 66.15000000001204228, -119.7731074845243739 ) ) ;
#123778=CARTESIAN_POINT ( 'NONE',  ( -16.87036670365548474, 65.91505003675672469, -115.5731074845243711 ) ) ;
#124044=EDGE_LOOP ( 'NONE', ( #170684, #112364, #68360, #53848 ) ) ;
#124417=CARTESIAN_POINT ( 'NONE',  ( -16.88783316861808359, 66.05000000001201954, -115.7753715265041308 ) ) ;
#124526=VERTEX_POINT ( 'NONE', #189668 ) ;
#124534=( LENGTH_UNIT ( ) NAMED_UNIT ( * ) SI_UNIT ( .MILLI., .METRE. ) );
#124880=VECTOR ( 'NONE', #77942, 1000.000000000000000 ) ;
#124935=PLANE ( 'NONE',  #122421 ) ;
#125009=CARTESIAN_POINT ( 'NONE',  ( -17.05016517656072139, 66.05000000001207638, -123.8504094885256706 ) ) ;
#125066=DIRECTION ( 'NONE',  ( 0.000000000000000000, 0.9553114395362733990, 0.2956011730205631016 ) ) ;
#125120=CARTESIAN_POINT ( 'NONE',  ( -16.81744102076748959, 66.05000000001201954, -115.6731074845243796 ) ) ;
#125388=CARTESIAN_POINT ( 'NONE',  ( -16.89081410710458542, 66.04868147016489388, -115.6687015646880070 ) ) ;
#125687=DIRECTION ( 'NONE',  ( -1.652117596168391700E-15, 1.000000000000000000, 6.982962677686266711E-15 ) ) ;
#125732=CARTESIAN_POINT ( 'NONE',  ( -13.43673303185029333, 66.55335100938319215, -121.4339441886011883 ) ) ;
#125756=DIRECTION ( 'NONE',  ( 1.000000000000000000, 0.000000000000000000, 0.000000000000000000 ) ) ;
#125959=VECTOR ( 'NONE', #155510, 1000.000000000000000 ) ;
#126170=ORIENTED_EDGE ( 'NONE', *, *, #52621, .T. ) ;
#126186=PLANE ( 'NONE',  #128066 ) ;
#126211=EDGE_CURVE ( 'NONE', #107243, #162266, #214826, .T. ) ;
#126232=ORIENTED_EDGE ( 'NONE', *, *, #170683, .F. ) ;
#126601=ADVANCED_FACE ( 'NONE', ( #96524 ), #181244, .F. ) ;
#126624=CIRCLE ( 'NONE', #1528, 1.749999999999999778 ) ;
#126855=ORIENTED_EDGE ( 'NONE', *, *, #169238, .T. ) ;
#126895=CARTESIAN_POINT ( 'NONE',  ( -18.34374000495059676, 64.52683809664949877, -112.2731074845243739 ) ) ;
#126903=CIRCLE ( 'NONE', #114430, 0.1000000000000028644 ) ;
#126976=CARTESIAN_POINT ( 'NONE',  ( -16.80621392010915471, 66.05779742250425102, -115.7126994499414820 ) ) ;
#127138=ADVANCED_FACE ( 'NONE', ( #141768 ), #7394, .F. ) ;
#127261=FACE_OUTER_BOUND ( 'NONE', #199642, .T. ) ;
#127391=VERTEX_POINT ( 'NONE', #83707 ) ;
#127414=VERTEX_POINT ( 'NONE', #253705 ) ;
#127567=CARTESIAN_POINT ( 'NONE',  ( -16.97092634996618798, 65.99911103366422083, -123.8929647182264944 ) ) ;
#127678=CARTESIAN_POINT ( 'NONE',  ( -16.77828822459933633, 66.05377062495554696, -115.6857357354433162 ) ) ;
#127752=AXIS2_PLACEMENT_3D ( 'NONE', #188256, #89146, #168751 ) ;
#127832=CARTESIAN_POINT ( 'NONE',  ( -18.40000000000000213, 64.51332499825441857, -127.2731074845243882 ) ) ;
#127924=DIRECTION ( 'NONE',  ( 1.000000000000000000, -1.186688945009009831E-16, -8.286604613020806758E-31 ) ) ;
#128066=AXIS2_PLACEMENT_3D ( 'NONE', #247420, #68805, #205726 ) ;
#128157=EDGE_CURVE ( 'NONE', #130548, #212715, #16766, .T. ) ;
#128165=CYLINDRICAL_SURFACE ( 'NONE', #254564, 0.5000000000000004441 ) ;
#128172=CARTESIAN_POINT ( 'NONE',  ( -16.27683809663751191, 66.65000000001208491, -123.9731074845243626 ) ) ;
#128258=CARTESIAN_POINT ( 'NONE',  ( -16.80070461187861142, 66.05000000001206217, -123.8761436553653397 ) ) ;
#128395=DIRECTION ( 'NONE',  ( 1.000000000000000000, -1.186688945009010077E-16, -8.286604613020808509E-31 ) ) ;
#128460=ORIENTED_EDGE ( 'NONE', *, *, #29325, .T. ) ;
#128689=ORIENTED_EDGE ( 'NONE', *, *, #205441, .F. ) ;
#128761=EDGE_CURVE ( 'NONE', #51212, #30385, #13592, .T. ) ;
#128864=B_SPLINE_CURVE_WITH_KNOTS ( 'NONE', 3,
 ( #44926, #60610, #240554, #234794, #209122, #68346, #210432, #47465, #8372, #227402, #167465, #246961, #245690, #87869, #129598, #26663, #125732, #147884, #48764, #30516, #91753, #27961, #107460, #206563, #31812, #190884 ),
 .UNSPECIFIED., .F., .F.,
 ( 4, 2, 2, 2, 2, 2, 2, 2, 2, 2, 2, 2, 4 ),
 ( 0.005476422646581359521, 0.006160811967703593017, 0.006845201288825827381, 0.007187395949386929384, 0.007529590609948032254, 0.007871785270509135124, 0.008213979931070237994, 0.008556174591631339130, 0.008898369252192442000, 0.009240563912753543135, 0.009582758573314646006, 0.01026714789443684828, 0.01095153721555904881 ),
 .UNSPECIFIED. ) ;
#128891=ORIENTED_EDGE ( 'NONE', *, *, #208436, .F. ) ;
#128938=ORIENTED_EDGE ( 'NONE', *, *, #110300, .T. ) ;
#129375=B_SPLINE_CURVE_WITH_KNOTS ( 'NONE', 3,
 ( #243216, #3311, #41209, #22925, #141557, #181979, #120748, #102398, #200254, #222348 ),
 .UNSPECIFIED., .F., .F.,
 ( 4, 3, 3, 4 ),
 ( 0.000000000000000000, 4.874959354401577961E-05, 9.785140065119720494E-05, 0.0001360444631935916505 ),
 .UNSPECIFIED. ) ;
#129541=CARTESIAN_POINT ( 'NONE',  ( -16.87683809663752399, 66.15000000001208491, -123.1207434663278804 ) ) ;
#129598=CARTESIAN_POINT ( 'NONE',  ( -13.77178122865954180, 66.54397173950414413, -121.5119094494586847 ) ) ;
#130056=CARTESIAN_POINT ( 'NONE',  ( 21.13736287352038445, 67.95335762362807941, -127.2731074845243597 ) ) ;
#130490=CARTESIAN_POINT ( 'NONE',  ( -16.94107738177414291, 65.98576071487538286, -115.5731074845243711 ) ) ;
#130548=VERTEX_POINT ( 'NONE', #109531 ) ;
#130775=CARTESIAN_POINT ( 'NONE',  ( 15.52844286134407525, 66.62433047358628357, -120.6553174751384461 ) ) ;
#130812=CARTESIAN_POINT ( 'NONE',  ( -16.79270642812296188, 66.05375578307388196, -123.8620407630872648 ) ) ;
#130844=CARTESIAN_POINT ( 'NONE',  ( -16.90128866880176162, 66.04620422280905245, -115.6604313011357306 ) ) ;
#130862=FACE_OUTER_BOUND ( 'NONE', #132653, .T. ) ;
#131033=ORIENTED_EDGE ( 'NONE', *, *, #169238, .F. ) ;
#131053=ORIENTED_EDGE ( 'NONE', *, *, #4620, .F. ) ;
#131530=DIRECTION ( 'NONE',  ( -1.000000000000000000, 0.000000000000000000, 0.000000000000000000 ) ) ;
#131557=FACE_OUTER_BOUND ( 'NONE', #207185, .T. ) ;
#131788=DIRECTION ( 'NONE',  ( 1.073024830501117725E-15, 6.982962677686266711E-15, -1.000000000000000000 ) ) ;
#132025=CARTESIAN_POINT ( 'NONE',  ( -16.77683809663752257, 66.05416425680790837, -123.8591584654201512 ) ) ;
#132064=CARTESIAN_POINT ( 'NONE',  ( 12.25000000000000000, 66.65000000001204228, -119.7731074845243739 ) ) ;
#132338=B_SPLINE_CURVE_WITH_KNOTS ( 'NONE', 3,
 ( #251356, #119245, #21442, #72765, #198757, #20143, #250085, #183068, #24005, #5672, #4407, #26569, #225996, #66957, #162235, #222151 ),
 .UNSPECIFIED., .F., .F.,
 ( 4, 3, 3, 3, 3, 4 ),
 ( 0.000000000000000000, 1.810570668010599751E-05, 2.740575833571215353E-05, 4.256816319435558806E-05, 5.213463471025249507E-05, 6.641585710717949479E-05 ),
 .UNSPECIFIED. ) ;
#132482=CARTESIAN_POINT ( 'NONE',  ( -17.01825945287481545, 66.05000000001201954, -115.7731074845243597 ) ) ;
#132653=EDGE_LOOP ( 'NONE', ( #26408, #221420, #180559, #251788 ) ) ;
#132674=EDGE_CURVE ( 'NONE', #187202, #17763, #104553, .T. ) ;
#132724=ORIENTED_EDGE ( 'NONE', *, *, #163986, .T. ) ;
#132734=VECTOR ( 'NONE', #180449, 1000.000000000000000 ) ;
#132850=EDGE_CURVE ( 'NONE', #164668, #130548, #11320, .T. ) ;
#132875=PLANE ( 'NONE',  #138396 ) ;
#132975=CARTESIAN_POINT ( 'NONE',  ( -16.81095280782811230, 66.05000000001207638, -123.8731074845252493 ) ) ;
#133046=FACE_OUTER_BOUND ( 'NONE', #103386, .T. ) ;
#133326=ORIENTED_EDGE ( 'NONE', *, *, #172165, .T. ) ;
#133351=ORIENTED_EDGE ( 'NONE', *, *, #170819, .T. ) ;
#133356=CARTESIAN_POINT ( 'NONE',  ( 14.56326696814971200, 66.55335100938319215, -121.4339441886011883 ) ) ;
#133437=CARTESIAN_POINT ( 'NONE',  ( -16.87036670365548474, 66.01058118071034642, -115.5435473672223168 ) ) ;
#133703=CARTESIAN_POINT ( 'NONE',  ( -16.87331047859651179, 66.05000000001207638, -123.8731074845243683 ) ) ;
#133827=CARTESIAN_POINT ( 'NONE',  ( -16.91256925476571382, 66.01426884188389010, -123.9907499735296454 ) ) ;
#133941=CARTESIAN_POINT ( 'NONE',  ( 12.60873083341396672, 66.61042836546560864, -118.7054667721552477 ) ) ;
#133996=CARTESIAN_POINT ( 'NONE',  ( -16.93230518875208190, 65.99924963859221805, -123.9473291364228658 ) ) ;
#134103=CARTESIAN_POINT ( 'NONE',  ( 18.39999999999999503, 64.25000000001199396, -112.2731074845243739 ) ) ;
#134172=FACE_OUTER_BOUND ( 'NONE', #150223, .T. ) ;
#134373=CARTESIAN_POINT ( 'NONE',  ( -16.83199318825828072, 66.06935387203084531, -115.7955222963151698 ) ) ;
#134378=DIRECTION ( 'NONE',  ( -1.073024830501117725E-15, 6.982962677686266711E-15, -1.000000000000000000 ) ) ;
#134723=CARTESIAN_POINT ( 'NONE',  ( -18.39999999999999858, 64.52683809664961245, -127.1971614177164156 ) ) ;
#135160=DIRECTION ( 'NONE',  ( 0.000000000000000000, 0.000000000000000000, 1.000000000000000000 ) ) ;
#135218=CARTESIAN_POINT ( 'NONE',  ( 14.22916352759893854, 66.54258906972185628, -118.0231915757780570 ) ) ;
#135265=CARTESIAN_POINT ( 'NONE',  ( -23.25000000000000355, 64.25000000001210765, -127.2731074845243882 ) ) ;
#135268=CARTESIAN_POINT ( 'NONE',  ( -16.93909480342659890, 66.00692163521051725, -123.9227604678520436 ) ) ;
#135332=AXIS2_PLACEMENT_3D ( 'NONE', #173337, #72935, #252804 ) ;
#135417=VERTEX_POINT ( 'NONE', #71986 ) ;
#135502=( BOUNDED_CURVE ( )  B_SPLINE_CURVE ( 3, ( #228571, #70799, #49915, #126895 ),
 .UNSPECIFIED., .F., .T. ) 
 B_SPLINE_CURVE_WITH_KNOTS ( ( 4, 4 ),
 ( 0.3000847527772386725, 0.5517402753107893965 ),
 .UNSPECIFIED. ) 
 CURVE ( )  GEOMETRIC_REPRESENTATION_ITEM ( )  RATIONAL_B_SPLINE_CURVE ( ( 1.000000000000000000, 0.9947294176030464508, 0.9947294176030464508, 1.000000000000000000 ) ) 
 REPRESENTATION_ITEM ( '' )  );
#135653=CARTESIAN_POINT ( 'NONE',  ( -16.93658623642905070, 66.01961832835493738, -123.9112047553951328 ) ) ;
#135709=EDGE_CURVE ( 'NONE', #32814, #204362, #126624, .T. ) ;
#135837=ORIENTED_EDGE ( 'NONE', *, *, #120799, .F. ) ;
#135910=ORIENTED_EDGE ( 'NONE', *, *, #6350, .F. ) ;
#135966=CARTESIAN_POINT ( 'NONE',  ( -16.94275863006528482, 66.01050395134448934, -115.6314101024477878 ) ) ;
#136495=CARTESIAN_POINT ( 'NONE',  ( 15.75000000000000000, 66.65000000001204228, -119.6573643172504973 ) ) ;
#136933=EDGE_LOOP ( 'NONE', ( #214082, #149416, #94485, #47967, #25066 ) ) ;
#137162=CARTESIAN_POINT ( 'NONE',  ( -16.80468759584937288, 66.05784632487790020, -123.8330886183227477 ) ) ;
#137176=AXIS2_PLACEMENT_3D ( 'NONE', #71776, #47031, #87449 ) ;
#137178=CARTESIAN_POINT ( 'NONE',  ( -21.65000000000000213, 68.75000000001202238, -115.6731074845243512 ) ) ;
#137186=CARTESIAN_POINT ( 'NONE',  ( -20.65000000000000568, 70.35000000001201670, -115.6731074845243370 ) ) ;
#137275=FACE_OUTER_BOUND ( 'NONE', #124044, .T. ) ;
#137361=EDGE_LOOP ( 'NONE', ( #146418, #15794, #185155, #252196 ) ) ;
#138160=B_SPLINE_CURVE_WITH_KNOTS ( 'NONE', 3,
 ( #23358, #102835, #98974, #186262 ),
 .UNSPECIFIED., .F., .F.,
 ( 4, 4 ),
 ( 0.000000000000000000, 7.713889350928753320E-05 ),
 .UNSPECIFIED. ) ;
#138163=AXIS2_PLACEMENT_3D ( 'NONE', #114470, #153658, #195321 ) ;
#138396=AXIS2_PLACEMENT_3D ( 'NONE', #212417, #191585, #110728 ) ;
#138405=DIRECTION ( 'NONE',  ( 1.000000000000000000, 0.000000000000000000, 0.000000000000000000 ) ) ;
#139039=ORIENTED_EDGE ( 'NONE', *, *, #14773, .F. ) ;
#139045=CARTESIAN_POINT ( 'NONE',  ( 15.39170923737819763, 66.61047060254530550, -118.7059995716306986 ) ) ;
#139093=CARTESIAN_POINT ( 'NONE',  ( -16.88560720703333473, 66.04943515626236206, -123.8749955636606472 ) ) ;
#139196=ORIENTED_EDGE ( 'NONE', *, *, #16754, .F. ) ;
#140027=FILL_AREA_STYLE_COLOUR ( '', #114862 ) ;
#140371=PLANE ( 'NONE',  #87830 ) ;
#140537=ORIENTED_EDGE ( 'NONE', *, *, #64090, .F. ) ;
#140616=CIRCLE ( 'NONE', #28234, 0.1999999999999987899 ) ;
#140713=EDGE_CURVE ( 'NONE', #198087, #37506, #112653, .T. ) ;
#140757=CLOSED_SHELL ( 'NONE', ( #235431, #232580, #73815, #216014, #26053, #2718, #34959, #188571, #114335, #85099, #211480, #225308, #194841, #3836, #150412, #17334, #54791, #249665, #192960, #116637, #155794, #53487, #181783, #127138, #60856, #36856, #1233, #153096, #12720, #119646, #56782, #154050, #204025, #247071, #153873, #60937, #56974, #149848, #174546, #155233, #211945, #60921, #46006, #126601, #77378, #159074, #227503, #201291, #108653, #199151, #60985, #9591, #98422 ) ) ;
#141335=SURFACE_SIDE_STYLE ('',( #119215 ) ) ;
#141557=CARTESIAN_POINT ( 'NONE',  ( -16.86422026484316916, 66.02955263915140449, -123.9408942588513725 ) ) ;
#141573=CARTESIAN_POINT ( 'NONE',  ( -16.87036670365549540, 66.01058118071040326, -124.0026676018264311 ) ) ;
#141592=ORIENTED_EDGE ( 'NONE', *, *, #132850, .F. ) ;
#141768=FACE_OUTER_BOUND ( 'NONE', #75954, .T. ) ;
#141884=DIRECTION ( 'NONE',  ( 1.186688945009009831E-16, 1.000000000000000000, 6.982962677686266711E-15 ) ) ;
#141941=LINE ( 'NONE', #98938, #157345 ) ;
#141946=ORIENTED_EDGE ( 'NONE', *, *, #254331, .F. ) ;
#142172=VECTOR ( 'NONE', #160421, 1000.000000000000000 ) ;
#142498=ORIENTED_EDGE ( 'NONE', *, *, #6008, .F. ) ;
#142568=DIRECTION ( 'NONE',  ( 0.000000000000000000, -6.982962677686266711E-15, 1.000000000000000000 ) ) ;
#142620=EDGE_CURVE ( 'NONE', #66849, #18395, #247733, .T. ) ;
#142736=DIRECTION ( 'NONE',  ( -1.073024830501117725E-15, -6.982962677686266711E-15, 1.000000000000000000 ) ) ;
#143066=VECTOR ( 'NONE', #97592, 1000.000000000000000 ) ;
#143067=VERTEX_POINT ( 'NONE', #231727 ) ;
#143583=DIRECTION ( 'NONE',  ( -0.000000000000000000, -6.982962677686266711E-15, 1.000000000000000000 ) ) ;
#143625=CIRCLE ( 'NONE', #64521, 14.30833333333333890 ) ;
#143822=B_SPLINE_CURVE_WITH_KNOTS ( 'NONE', 3,
 ( #87547, #27632, #227065, #246630, #184094, #108420, #229650, #65430, #185382, #228370 ),
 .UNSPECIFIED., .F., .F.,
 ( 4, 2, 2, 2, 4 ),
 ( 0.000000000000000000, 0.0003916577441626822214, 0.0005874866162440240368, 0.0006854010522846949987, 0.0007833154883253658522 ),
 .UNSPECIFIED. ) ;
#144136=EDGE_CURVE ( 'NONE', #175330, #127414, #230410, .T. ) ;
#144210=EDGE_CURVE ( 'NONE', #64183, #78597, #3328, .T. ) ;
#144297=AXIS2_PLACEMENT_3D ( 'NONE', #189434, #167318, #70790 ) ;
#144523=VERTEX_POINT ( 'NONE', #236514 ) ;
#144808=CARTESIAN_POINT ( 'NONE',  ( 17.23472005113828232, 65.69211804551129319, -125.0696843445930568 ) ) ;
#144882=CARTESIAN_POINT ( 'NONE',  ( 18.54999999999999716, 67.25000000001197975, -115.6731074845243654 ) ) ;
#144983=DIRECTION ( 'NONE',  ( 1.000000000000000000, 0.000000000000000000, 0.000000000000000000 ) ) ;
#145021=CARTESIAN_POINT ( 'NONE',  ( -18.40000000000000213, 64.58541674041228475, -123.8731074845243683 ) ) ;
#145158=EDGE_LOOP ( 'NONE', ( #37127, #62844, #114052 ) ) ;
#145179=VECTOR ( 'NONE', #18567, 1000.000000000000000 ) ;
#145427=ORIENTED_EDGE ( 'NONE', *, *, #224428, .T. ) ;
#145454=CARTESIAN_POINT ( 'NONE',  ( 23.24999999999999645, 67.17743825834560312, -115.6731074845243654 ) ) ;
#145550=VECTOR ( 'NONE', #191077, 1000.000000000000000 ) ;
#145653=ORIENTED_EDGE ( 'NONE', *, *, #117380, .F. ) ;
#145785=FACE_OUTER_BOUND ( 'NONE', #200707, .T. ) ;
#146068=ORIENTED_EDGE ( 'NONE', *, *, #171361, .F. ) ;
#146169=CARTESIAN_POINT ( 'NONE',  ( -12.25000000000000178, 66.15000000001204228, -119.7731074845243739 ) ) ;
#146418=ORIENTED_EDGE ( 'NONE', *, *, #40766, .F. ) ;
#146630=( NAMED_UNIT ( * ) PLANE_ANGLE_UNIT ( ) SI_UNIT ( $, .RADIAN. ) );
#146704=ORIENTED_EDGE ( 'NONE', *, *, #132674, .T. ) ;
#146717=CARTESIAN_POINT ( 'NONE',  ( -18.39999999999999858, 64.52683809664961245, -127.1971614177164156 ) ) ;
#146722=AXIS2_PLACEMENT_3D ( 'NONE', #5716, #106101, #125687 ) ;
#146750=CARTESIAN_POINT ( 'NONE',  ( -16.97683809663752186, 66.05000000001207638, -123.1207434663278804 ) ) ;
#146753=LINE ( 'NONE', #105044, #107281 ) ;
#146879=VECTOR ( 'NONE', #221176, 1000.000000000000000 ) ;
#147092=CARTESIAN_POINT ( 'NONE',  ( -18.40000000000000213, 70.35000000001207354, -123.8731074845243398 ) ) ;
#147113=CARTESIAN_POINT ( 'NONE',  ( -17.04295772865479464, 65.97510057475051326, -123.8731074845243683 ) ) ;
#147174=CARTESIAN_POINT ( 'NONE',  ( -15.55912972643740488, 67.50912972644943011, -115.6731074845243654 ) ) ;
#147227=ORIENTED_EDGE ( 'NONE', *, *, #237023, .T. ) ;
#147526=CARTESIAN_POINT ( 'NONE',  ( -17.71734398241074615, 65.15764277154752904, -126.2482457375299560 ) ) ;
#147788=CARTESIAN_POINT ( 'NONE',  ( 14.22821877134046176, 66.54397173950412991, -121.5119094494586420 ) ) ;
#147825=CARTESIAN_POINT ( 'NONE',  ( -16.84981964351479178, 66.08268176591337806, -123.6535058705048726 ) ) ;
#147835=CARTESIAN_POINT ( 'NONE',  ( -16.77308656112214535, 66.05000000001201954, -115.6733006762266598 ) ) ;
#147884=CARTESIAN_POINT ( 'NONE',  ( -13.22483237240078502, 66.56332574816921976, -121.3462455535252076 ) ) ;
#147944=PRESENTATION_STYLE_ASSIGNMENT (( #85358 ) ) ;
#148042=EDGE_CURVE ( 'NONE', #240802, #10416, #197649, .T. ) ;
#148137=CARTESIAN_POINT ( 'NONE',  ( -16.92507428761700439, 66.05000000001207638, -123.8097100249028131 ) ) ;
#148165=STYLED_ITEM ( 'NONE', ( #120520 ), #119926 ) ;
#148271=EDGE_CURVE ( 'NONE', #154055, #39978, #51354, .T. ) ;
#148569=CARTESIAN_POINT ( 'NONE',  ( -18.36973785203555920, 64.52449679952776762, -112.2731074845243739 ) ) ;
#148778=DIRECTION ( 'NONE',  ( 1.186688945009009831E-16, 1.000000000000000000, 6.982962677686266711E-15 ) ) ;
#148805=CARTESIAN_POINT ( 'NONE',  ( -16.87665923198281348, 66.05000000001201954, -115.6731074845243796 ) ) ;
#148825=CARTESIAN_POINT ( 'NONE',  ( -17.22361732159832215, 65.65484434140965675, -125.1523229586572512 ) ) ;
#148868=CARTESIAN_POINT ( 'NONE',  ( -17.29158576265543346, 65.63525233399408876, -114.4403492397321997 ) ) ;
#149140=( BOUNDED_SURFACE ( )  B_SPLINE_SURFACE ( 3, 2, ( 
 ( #130490, #108379, #110936 ),
 ( #190503, #186640, #206188 ),
 ( #11866, #210056, #168399 ),
 ( #8001, #109640, #91383 ) ),
 .UNSPECIFIED., .F., .F., .T. ) 
 B_SPLINE_SURFACE_WITH_KNOTS ( ( 4, 4 ),
 ( 3, 3 ),
 ( 0.3000847527772385059, 0.5552748953338751958 ),
 ( 0.000000000000000000, 1.000000000000000000 ),
 .UNSPECIFIED. ) 
 GEOMETRIC_REPRESENTATION_ITEM ( )  RATIONAL_B_SPLINE_SURFACE ( (
 ( 1.000000000000000000, 0.9152888060719408525, 1.000000000000000000),
 ( 1.000000000000000000, 0.9104333467450372863, 1.000000000000000000),
 ( 1.000000000000000000, 0.9035312726220605661, 1.000000000000000000),
 ( 1.000000000000000000, 0.8946697475932182675, 1.000000000000000000) ) ) 
 REPRESENTATION_ITEM ( '' )  SURFACE ( )  );
#149171=PLANE ( 'NONE',  #34271 ) ;
#149416=ORIENTED_EDGE ( 'NONE', *, *, #36456, .F. ) ;
#149695=CYLINDRICAL_SURFACE ( 'NONE', #191189, 1.749999999999999778 ) ;
#149848=ADVANCED_FACE ( 'NONE', ( #238760 ), #83497, .F. ) ;
#149927=VERTEX_POINT ( 'NONE', #118826 ) ;
#149972=( BOUNDED_CURVE ( )  B_SPLINE_CURVE ( 3, ( #1334, #99147, #79584, #17089 ),
 .UNSPECIFIED., .F., .F. ) 
 B_SPLINE_CURVE_WITH_KNOTS ( ( 4, 4 ),
 ( 1.289024775538054608E-13, 1.570796326794793529 ),
 .UNSPECIFIED. ) 
 CURVE ( )  GEOMETRIC_REPRESENTATION_ITEM ( )  RATIONAL_B_SPLINE_CURVE ( ( 1.000000000000000000, 0.8047378541244196715, 0.8047378541244196715, 1.000000000000000000 ) ) 
 REPRESENTATION_ITEM ( '' )  );
#150044=DIRECTION ( 'NONE',  ( 0.5932847527679310229, 0.8049926720990042694, 5.621233785078285907E-15 ) ) ;
#150223=EDGE_LOOP ( 'NONE', ( #195493, #192943, #10952, #223311, #108773, #107095, #242222, #221489, #77041, #115909, #71342, #35212, #112173, #8474 ) ) ;
#150357=CARTESIAN_POINT ( 'NONE',  ( 13.43443725621852991, 66.55344247693950877, -121.4331655301785133 ) ) ;
#150412=ADVANCED_FACE ( 'NONE', ( #224004 ), #126186, .F. ) ;
#150586=VERTEX_POINT ( 'NONE', #34508 ) ;
#151022=CARTESIAN_POINT ( 'NONE',  ( -15.55912972643741199, 67.50912972644950116, -123.8731074845243683 ) ) ;
#151175=CARTESIAN_POINT ( 'NONE',  ( -18.40000000000000213, 64.51332499825430489, -112.2731074845243739 ) ) ;
#151184=ORIENTED_EDGE ( 'NONE', *, *, #93395, .T. ) ;
#151260=CARTESIAN_POINT ( 'NONE',  ( 15.48841904831874849, 67.43841904833078615, -115.6731074845243654 ) ) ;
#151437=CARTESIAN_POINT ( 'NONE',  ( -16.94107738177414291, 65.98576071487538286, -115.5731074845243711 ) ) ;
#151592=DIRECTION ( 'NONE',  ( 0.000000000000000000, 6.982962677686266711E-15, -1.000000000000000000 ) ) ;
#151729=CARTESIAN_POINT ( 'NONE',  ( -16.94333152882356330, 66.00965798855433775, -115.6310759534228794 ) ) ;
#151758=EDGE_CURVE ( 'NONE', #70684, #191326, #64461, .T. ) ;
#152097=CARTESIAN_POINT ( 'NONE',  ( -16.87683809663752399, 66.15000000001201386, -116.4254715027206686 ) ) ;
#152348=FACE_OUTER_BOUND ( 'NONE', #41694, .T. ) ;
#152369=VERTEX_POINT ( 'NONE', #73167 ) ;
#152493=PLANE ( 'NONE',  #77345 ) ;
#152522=CARTESIAN_POINT ( 'NONE',  ( -16.97683809663752186, 66.05000000001210481, -127.2731074845243597 ) ) ;
#152541=DIRECTION ( 'NONE',  ( 1.000000000000000000, -1.646408749285562060E-14, -1.073024830501232702E-15 ) ) ;
#152595=EDGE_LOOP ( 'NONE', ( #38018, #33186, #12699, #12119 ) ) ;
#152715=ORIENTED_EDGE ( 'NONE', *, *, #56463, .T. ) ;
#152814=EDGE_CURVE ( 'NONE', #9830, #79879, #158806, .T. ) ;
#152949=CARTESIAN_POINT ( 'NONE',  ( 13.76927104934457624, 66.54401276639930529, -121.5115763176265347 ) ) ;
#153096=ADVANCED_FACE ( 'NONE', ( #9971 ), #89492, .F. ) ;
#153411=AXIS2_PLACEMENT_3D ( 'NONE', #201437, #142736, #239291 ) ;
#153513=CARTESIAN_POINT ( 'NONE',  ( 0.000000000000000000, 0.000000000000000000, 0.000000000000000000 ) ) ;
#153569=CARTESIAN_POINT ( 'NONE',  ( 12.48201962039795809, 66.62334006147848697, -118.8949149363070319 ) ) ;
#153658=DIRECTION ( 'NONE',  ( -0.7071067811865487940, -0.7071067811865463515, -4.937700262164522799E-15 ) ) ;
#153873=ADVANCED_FACE ( 'NONE', ( #131557 ), #29916, .F. ) ;
#153909=CARTESIAN_POINT ( 'NONE',  ( -15.75000000000000355, 66.65000000001204228, -119.7731074845243739 ) ) ;
#154050=ADVANCED_FACE ( 'NONE', ( #15483 ), #200514, .F. ) ;
#154055=VERTEX_POINT ( 'NONE', #44005 ) ;
#154191=EDGE_LOOP ( 'NONE', ( #101846, #40863, #187023, #111901 ) ) ;
#154457=DIRECTION ( 'NONE',  ( -1.000000000000000000, 0.000000000000000000, -0.000000000000000000 ) ) ;
#154491=LINE ( 'NONE', #34528, #191575 ) ;
#154601=LINE ( 'NONE', #55429, #102183 ) ;
#154732=CARTESIAN_POINT ( 'NONE',  ( 18.54999999999999716, 66.05000000001200533, -115.6731074845243228 ) ) ;
#154843=VECTOR ( 'NONE', #247870, 1000.000000000000000 ) ;
#154868=AXIS2_PLACEMENT_3D ( 'NONE', #135265, #156160, #17890 ) ;
#154977=VECTOR ( 'NONE', #64442, 1000.000000000000000 ) ;
#155100=ORIENTED_EDGE ( 'NONE', *, *, #46227, .T. ) ;
#155233=ADVANCED_FACE ( 'NONE', ( #220591 ), #217146, .T. ) ;
#155268=ORIENTED_EDGE ( 'NONE', *, *, #113023, .T. ) ;
#155298=VERTEX_POINT ( 'NONE', #144882 ) ;
#155403=EDGE_CURVE ( 'NONE', #30013, #159618, #249155, .T. ) ;
#155510=DIRECTION ( 'NONE',  ( 0.000000000000000000, -6.982962677686266711E-15, 1.000000000000000000 ) ) ;
#155604=AXIS2_PLACEMENT_3D ( 'NONE', #257083, #78480, #158084 ) ;
#155794=ADVANCED_FACE ( 'NONE', ( #170633 ), #250115, .F. ) ;
#155826=EDGE_CURVE ( 'NONE', #156548, #30013, #191461, .T. ) ;
#155964=CARTESIAN_POINT ( 'NONE',  ( -14.45422546970484312, 66.54939790392351995, -118.0792115214276947 ) ) ;
#156081=DIRECTION ( 'NONE',  ( 1.000000000000000000, 0.000000000000000000, 0.000000000000000000 ) ) ;
#156117=CARTESIAN_POINT ( 'NONE',  ( 12.25000000000000000, 66.65000000001205649, -119.6588398769083312 ) ) ;
#156120=DIRECTION ( 'NONE',  ( 1.000000000000000000, 0.000000000000000000, 0.000000000000000000 ) ) ;
#156160=DIRECTION ( 'NONE',  ( 0.000000000000000000, 1.000000000000000000, 6.982962677686266711E-15 ) ) ;
#156364=CARTESIAN_POINT ( 'NONE',  ( -16.87683809663752399, 66.15000000001205649, -123.1207434663280651 ) ) ;
#156375=ORIENTED_EDGE ( 'NONE', *, *, #221105, .F. ) ;
#156478=EDGE_CURVE ( 'NONE', #94366, #162266, #67770, .T. ) ;
#156548=VERTEX_POINT ( 'NONE', #90086 ) ;
#156563=CARTESIAN_POINT ( 'NONE',  ( -16.83794479845802883, 66.07364258066050411, -115.8266627803021009 ) ) ;
#156883=CARTESIAN_POINT ( 'NONE',  ( -16.91256925476570672, 66.01426884188381905, -115.5554649955190882 ) ) ;
#157250=CARTESIAN_POINT ( 'NONE',  ( -15.51798037960204546, 66.62334006147850118, -118.8949149363070887 ) ) ;
#157345=VECTOR ( 'NONE', #199372, 999.9999999999998863 ) ;
#157456=DIRECTION ( 'NONE',  ( -0.7071067811865487940, -0.7071067811865463515, -4.216150419019404490E-15 ) ) ;
#157547=CARTESIAN_POINT ( 'NONE',  ( -18.40000000000000213, 64.52683809664958403, -123.9731074845243768 ) ) ;
#157568=ORIENTED_EDGE ( 'NONE', *, *, #67932, .T. ) ;
#157609=DIRECTION ( 'NONE',  ( 1.000000000000000000, 0.000000000000000000, 0.000000000000000000 ) ) ;
#157685=LINE ( 'NONE', #73003, #219357 ) ;
#158084=DIRECTION ( 'NONE',  ( 0.000000000000000000, -6.982962677686266711E-15, 1.000000000000000000 ) ) ;
#158194=ORIENTED_EDGE ( 'NONE', *, *, #155403, .T. ) ;
#158215=LINE ( 'NONE', #59029, #208671 ) ;
#158231=VECTOR ( 'NONE', #4141, 1000.000000000000000 ) ;
#158442=DIRECTION ( 'NONE',  ( 0.000000000000000000, -1.000000000000000000, -6.982962677686266711E-15 ) ) ;
#158503=CARTESIAN_POINT ( 'NONE',  ( -18.40000000000000213, 64.25000000001199396, -112.2731074845243739 ) ) ;
#158806=LINE ( 'NONE', #177086, #124880 ) ;
#158902=CARTESIAN_POINT ( 'NONE',  ( -21.65000000000000213, 66.05000000001207638, -123.7731074845243739 ) ) ;
#158958=EDGE_CURVE ( 'NONE', #155298, #78597, #85963, .T. ) ;
#159074=ADVANCED_FACE ( 'NONE', ( #42468 ), #26561, .T. ) ;
#159275=CARTESIAN_POINT ( 'NONE',  ( 16.87683809663750267, 66.05000000001207638, -123.8731074845243683 ) ) ;
#159344=CYLINDRICAL_SURFACE ( 'NONE', #66191, 14.30833333333333890 ) ;
#159455=DIRECTION ( 'NONE',  ( -1.000000000000000000, 4.625929269271478222E-14, 0.000000000000000000 ) ) ;
#159618=VERTEX_POINT ( 'NONE', #40305 ) ;
#159667=LINE ( 'NONE', #202630, #167523 ) ;
#159775=CARTESIAN_POINT ( 'NONE',  ( 20.09999999999999787, 66.25000000001205080, -115.6731074845243796 ) ) ;
#159862=DIRECTION ( 'NONE',  ( 1.073024830501117725E-15, -6.982962677686266711E-15, 1.000000000000000000 ) ) ;
#160033=CARTESIAN_POINT ( 'NONE',  ( -23.25000000000000355, 70.35000000001207354, -123.8731074845243398 ) ) ;
#160421=DIRECTION ( 'NONE',  ( -0.000000000000000000, -6.982962677686266711E-15, 1.000000000000000000 ) ) ;
#160500=B_SPLINE_CURVE_WITH_KNOTS ( 'NONE', 3,
 ( #99973, #197815, #221219, #139093, #875, #23066, #80402, #118298, #59557, #239526 ),
 .UNSPECIFIED., .F., .F.,
 ( 4, 3, 3, 4 ),
 ( 1.957469226477651626E-15, 8.145022132840017156E-06, 1.905645951092857371E-05, 2.061107371226198839E-05 ),
 .UNSPECIFIED. ) ;
#160563=VECTOR ( 'NONE', #210138, 1000.000000000000000 ) ;
#160740=EDGE_CURVE ( 'NONE', #56104, #184009, #62583, .T. ) ;
#161150=CARTESIAN_POINT ( 'NONE',  ( -17.22767730083365123, 65.65075578754337471, -125.1655361750991204 ) ) ;
#161173=DIRECTION ( 'NONE',  ( -1.000000000000000000, 0.000000000000000000, -0.000000000000000000 ) ) ;
#161204=ORIENTED_EDGE ( 'NONE', *, *, #144210, .F. ) ;
#161787=ORIENTED_EDGE ( 'NONE', *, *, #229810, .T. ) ;
#161963=CARTESIAN_POINT ( 'NONE',  ( -16.77683809663752257, 66.05000000001201954, -115.6731074845243796 ) ) ;
#162235=CARTESIAN_POINT ( 'NONE',  ( -16.94132844910801339, 66.00756324483165827, -115.6269057285420558 ) ) ;
#162248=CARTESIAN_POINT ( 'NONE',  ( 18.39999999999997371, 64.52683809664949877, -112.2731074845243739 ) ) ;
#162266=VERTEX_POINT ( 'NONE', #240230 ) ;
#162445=CARTESIAN_POINT ( 'NONE',  ( -18.44085059012131822, 64.48598750652828926, -127.2634128036459202 ) ) ;
#162467=FACE_OUTER_BOUND ( 'NONE', #239751, .T. ) ;
#162645=CARTESIAN_POINT ( 'NONE',  ( 18.39999999999999503, 64.25000000001207923, -123.8731074845243683 ) ) ;
#162750=DIRECTION ( 'NONE',  ( 1.000000000000000000, 0.000000000000000000, 0.000000000000000000 ) ) ;
#162966=CARTESIAN_POINT ( 'NONE',  ( -16.77779411440718604, 66.05389855290439982, -115.6861649015288975 ) ) ;
#163260=CARTESIAN_POINT ( 'NONE',  ( -17.11825945287481332, 66.05000000001201954, -115.7731074845243597 ) ) ;
#163360=EDGE_CURVE ( 'NONE', #166838, #19374, #249861, .T. ) ;
#163439=VECTOR ( 'NONE', #79801, 1000.000000000000000 ) ;
#163519=CARTESIAN_POINT ( 'NONE',  ( 15.74999999999999645, 66.65000000001204228, -119.7731074845243739 ) ) ;
#163645=CARTESIAN_POINT ( 'NONE',  ( -15.75000000000000355, 66.65000000001204228, -119.7731074845243739 ) ) ;
#163825=CARTESIAN_POINT ( 'NONE',  ( 18.54999999999999716, 67.25000000001203659, -123.8731074845243683 ) ) ;
#163986=EDGE_CURVE ( 'NONE', #4154, #256392, #66959, .T. ) ;
#164018=DIRECTION ( 'NONE',  ( 1.000000000000000000, 0.000000000000000000, 0.000000000000000000 ) ) ;
#164104=EDGE_CURVE ( 'NONE', #256568, #7935, #206283, .T. ) ;
#164324=VECTOR ( 'NONE', #100192, 1000.000000000000000 ) ;
#164542=CARTESIAN_POINT ( 'NONE',  ( -16.87331047859649757, 66.05000000001201954, -115.6731074845243796 ) ) ;
#164638=B_SPLINE_CURVE_WITH_KNOTS ( 'NONE', 3,
 ( #58534, #132975, #16879, #53420, #35185, #13037, #174705, #39008, #237199, #232079, #191686, #192940, #36455 ),
 .UNSPECIFIED., .F., .F.,
 ( 4, 3, 3, 3, 4 ),
 ( 1.084445006577768341E-16, 1.946463881814499081E-05, 3.922356109944648083E-05, 4.215060953239448225E-05, 4.415117091092920593E-05 ),
 .UNSPECIFIED. ) ;
#164668=VERTEX_POINT ( 'NONE', #244450 ) ;
#164736=CARTESIAN_POINT ( 'NONE',  ( 23.24999999999999645, 70.35000000001207354, -123.8731074845243398 ) ) ;
#164825=CARTESIAN_POINT ( 'NONE',  ( -16.85697194749126027, 66.09145628588836985, -115.9581117521381657 ) ) ;
#164865=DIRECTION ( 'NONE',  ( 1.186688945009009831E-16, 1.000000000000000000, 6.982962677686266711E-15 ) ) ;
#164999=EDGE_LOOP ( 'NONE', ( #75731, #236330, #72445, #126855 ) ) ;
#165015=EDGE_CURVE ( 'NONE', #175330, #79626, #15713, .T. ) ;
#165198=CARTESIAN_POINT ( 'NONE',  ( 20.99999999999999645, 66.25000000001210765, -127.2731074845243597 ) ) ;
#165298=LINE ( 'NONE', #66203, #44238 ) ;
#165527=CARTESIAN_POINT ( 'NONE',  ( -16.80939487329394666, 66.05000000001201954, -115.6731074845234843 ) ) ;
#165599=ORIENTED_EDGE ( 'NONE', *, *, #140713, .F. ) ;
#165782=CARTESIAN_POINT ( 'NONE',  ( -14.00000000000000178, 66.15000000001204228, -119.7731074845243739 ) ) ;
#165879=AXIS2_PLACEMENT_3D ( 'NONE', #43133, #97928, #22301 ) ;
#165902=DIRECTION ( 'NONE',  ( 0.000000000000000000, -6.789366196018718420E-15, 1.000000000000000000 ) ) ;
#166464=ORIENTED_EDGE ( 'NONE', *, *, #198574, .F. ) ;
#166520=EDGE_LOOP ( 'NONE', ( #165599, #86066, #241039, #37006 ) ) ;
#166650=CARTESIAN_POINT ( 'NONE',  ( -21.65000000000000213, 68.75000000001207923, -123.8731074845243540 ) ) ;
#166715=ORIENTED_EDGE ( 'NONE', *, *, #87606, .F. ) ;
#166739=ORIENTED_EDGE ( 'NONE', *, *, #234663, .F. ) ;
#166834=CARTESIAN_POINT ( 'NONE',  ( -16.77732147262506146, 66.05403306739336244, -115.6866162412485011 ) ) ;
#166838=VERTEX_POINT ( 'NONE', #92528 ) ;
#166863=EDGE_CURVE ( 'NONE', #12698, #149927, #233368, .T. ) ;
#167104=DIRECTION ( 'NONE',  ( -1.000000000000000000, 0.000000000000000000, 0.000000000000000000 ) ) ;
#167318=DIRECTION ( 'NONE',  ( -1.000000000000000000, 1.186688945009010077E-16, 8.286604613020808509E-31 ) ) ;
#167402=CARTESIAN_POINT ( 'NONE',  ( -16.83558968593870020, 66.05000000001207638, -123.8608022969078775 ) ) ;
#167411=CARTESIAN_POINT ( 'NONE',  ( -16.80891096016330977, 66.05000000001201954, -115.6554446772562272 ) ) ;
#167465=CARTESIAN_POINT ( 'NONE',  ( -14.45443560709636444, 66.54940788787834549, -121.4669191657159644 ) ) ;
#167523=VECTOR ( 'NONE', #223466, 1000.000000000000000 ) ;
#167530=SURFACE_SIDE_STYLE ('',( #50113 ) ) ;
#167658=EDGE_CURVE ( 'NONE', #5646, #105369, #84450, .T. ) ;
#168016=CARTESIAN_POINT ( 'NONE',  ( -16.91049119928363353, 66.05000000001209060, -123.9048278777151921 ) ) ;
#168173=CARTESIAN_POINT ( 'NONE',  ( -18.38817693311004575, 64.51850848411221762, -112.2731074845243739 ) ) ;
#168335=CYLINDRICAL_SURFACE ( 'NONE', #137176, 0.1999999999999987899 ) ;
#168352=DIRECTION ( 'NONE',  ( -0.8049926720990042694, 0.5932847527679310229, 4.142885285818786163E-15 ) ) ;
#168399=CARTESIAN_POINT ( 'NONE',  ( -17.73285935859749074, 65.14201819621466427, -113.2645456747330002 ) ) ;
#168427=CARTESIAN_POINT ( 'NONE',  ( -16.87036670365549895, 66.01058118071041747, -124.0026676018264169 ) ) ;
#168642=CARTESIAN_POINT ( 'NONE',  ( -17.04761207306819060, 65.97354912661430149, -123.8731074845243683 ) ) ;
#168751=DIRECTION ( 'NONE',  ( 0.000000000000000000, -6.982962677686266711E-15, 1.000000000000000000 ) ) ;
#168778=ORIENTED_EDGE ( 'NONE', *, *, #46227, .F. ) ;
#168834=( NAMED_UNIT ( * ) SI_UNIT ( $, .STERADIAN. ) SOLID_ANGLE_UNIT ( ) );
#169027=DIRECTION ( 'NONE',  ( 1.073024830501117725E-15, -6.982962677686266711E-15, 1.000000000000000000 ) ) ;
#169087=CARTESIAN_POINT ( 'NONE',  ( 18.39999999999999503, 70.35000000001200249, -112.2731074845243313 ) ) ;
#169118=EDGE_CURVE ( 'NONE', #241136, #198612, #76763, .T. ) ;
#169225=FACE_OUTER_BOUND ( 'NONE', #225264, .T. ) ;
#169238=EDGE_CURVE ( 'NONE', #149927, #154055, #101187, .T. ) ;
#169527=VECTOR ( 'NONE', #189067, 1000.000000000000000 ) ;
#169545=CARTESIAN_POINT ( 'NONE',  ( 15.74999999999999645, 66.15000000001204228, -119.7731074845243739 ) ) ;
#169636=PLANE ( 'NONE',  #87966 ) ;
#169752=LINE ( 'NONE', #112320, #160563 ) ;
#169771=DIRECTION ( 'NONE',  ( 1.000000000000000000, 0.000000000000000000, 0.000000000000000000 ) ) ;
#169992=CARTESIAN_POINT ( 'NONE',  ( -16.80621392010908011, 66.05779742250423681, -123.8335155191076211 ) ) ;
#170039=CARTESIAN_POINT ( 'NONE',  ( -16.89268316805466341, 66.04827818676987761, -123.8788599630699281 ) ) ;
#170140=ORIENTED_EDGE ( 'NONE', *, *, #198574, .T. ) ;
#170383=DIRECTION ( 'NONE',  ( -1.000000000000000000, 0.000000000000000000, -0.000000000000000000 ) ) ;
#170611=( BOUNDED_CURVE ( )  B_SPLINE_CURVE ( 3, ( #82353, #257123, #98062, #240193 ),
 .UNSPECIFIED., .F., .T. ) 
 B_SPLINE_CURVE_WITH_KNOTS ( ( 4, 4 ),
 ( 3.752122642744585068, 4.712388980384675463 ),
 .UNSPECIFIED. ) 
 CURVE ( )  GEOMETRIC_REPRESENTATION_ITEM ( )  RATIONAL_B_SPLINE_CURVE ( ( 1.000000000000000000, 0.9246222802177217481, 0.9246222802177217481, 1.000000000000000000 ) ) 
 REPRESENTATION_ITEM ( '' )  );
#170624=CARTESIAN_POINT ( 'NONE',  ( -18.40000000000000213, 64.51332499825441857, -127.2731074845243882 ) ) ;
#170633=FACE_OUTER_BOUND ( 'NONE', #204328, .T. ) ;
#170683=EDGE_CURVE ( 'NONE', #127414, #150586, #118203, .T. ) ;
#170684=ORIENTED_EDGE ( 'NONE', *, *, #49941, .T. ) ;
#170819=EDGE_CURVE ( 'NONE', #181057, #90904, #31883, .T. ) ;
#170857=ORIENTED_EDGE ( 'NONE', *, *, #249609, .T. ) ;
#171031=ORIENTED_EDGE ( 'NONE', *, *, #243562, .T. ) ;
#171361=EDGE_CURVE ( 'NONE', #14308, #181057, #70791, .T. ) ;
#171384=EDGE_CURVE ( 'NONE', #135417, #51212, #227258, .T. ) ;
#171439=VECTOR ( 'NONE', #238320, 1000.000000000000000 ) ;
#171440=AXIS2_PLACEMENT_3D ( 'NONE', #109411, #188966, #32501 ) ;
#171887=CARTESIAN_POINT ( 'NONE',  ( -16.94309007106720344, 66.00777380744206368, -123.9173162019688732 ) ) ;
#172021=CARTESIAN_POINT ( 'NONE',  ( -18.40000000000000213, 64.51332499825430489, -112.2731074845243739 ) ) ;
#172165=EDGE_CURVE ( 'NONE', #256630, #164668, #138160, .T. ) ;
#172234=ORIENTED_EDGE ( 'NONE', *, *, #234663, .T. ) ;
#172266=EDGE_LOOP ( 'NONE', ( #106529, #235611 ) ) ;
#172289=CARTESIAN_POINT ( 'NONE',  ( -23.25000000000000355, 70.35000000001210196, -127.2731074845243313 ) ) ;
#172353=PRODUCT ( 'Snap Open Cable Crossbars 13', 'Snap Open Cable Crossbars 13', '', ( #71807 ) ) ;
#172450=ORIENTED_EDGE ( 'NONE', *, *, #6282, .T. ) ;
#172482=DIRECTION ( 'NONE',  ( 0.7071067811865463515, 0.7071067811865487940, 4.937700262164540154E-15 ) ) ;
#172614=CARTESIAN_POINT ( 'NONE',  ( -16.94878442675511465, 66.00827089702099215, -115.6348879088864976 ) ) ;
#172636=EDGE_CURVE ( 'NONE', #119280, #55681, #25948, .T. ) ;
#172705=CARTESIAN_POINT ( 'NONE',  ( 18.39999999999999503, 64.52683809664958403, -123.8731074845243683 ) ) ;
#172886=CARTESIAN_POINT ( 'NONE',  ( -16.92209698673680052, 66.05000000001201954, -115.7337430515765533 ) ) ;
#172887=DIRECTION ( 'NONE',  ( -1.000000000000000000, -1.652117596168391700E-15, -1.153667551319263085E-29 ) ) ;
#173133=CARTESIAN_POINT ( 'NONE',  ( 12.84435279558020149, 66.58929125296495499, -118.4538990786802941 ) ) ;
#173186=DIRECTION ( 'NONE',  ( 1.020425574104004196E-15, 6.982962677686266711E-15, -1.000000000000000000 ) ) ;
#173232=ORIENTED_EDGE ( 'NONE', *, *, #14773, .T. ) ;
#173337=CARTESIAN_POINT ( 'NONE',  ( -21.64999999999999858, 65.95000000001206786, -123.7731074845243739 ) ) ;
#173633=CARTESIAN_POINT ( 'NONE',  ( -16.87304349924914604, 66.03825492205483272, -115.6340408094791172 ) ) ;
#173772=CARTESIAN_POINT ( 'NONE',  ( 23.24999999999999645, 67.17743825834565996, -123.8731074845243683 ) ) ;
#173879=CARTESIAN_POINT ( 'NONE',  ( -16.94445028196807002, 66.00793639031427062, -115.6304376629428106 ) ) ;
#173989=DIRECTION ( 'NONE',  ( 1.020425574104004196E-15, -6.982962677686266711E-15, 1.000000000000000000 ) ) ;
#174266=CARTESIAN_POINT ( 'NONE',  ( -13.11924609551135212, 66.56831044948793874, -118.2438174522883116 ) ) ;
#174289=DIRECTION ( 'NONE',  ( 0.000000000000000000, 1.000000000000000000, 6.982962677686266711E-15 ) ) ;
#174421=DIRECTION ( 'NONE',  ( 0.000000000000000000, -6.982962677686266711E-15, 1.000000000000000000 ) ) ;
#174469=CARTESIAN_POINT ( 'NONE',  ( -16.93262454970420094, 65.99797953208170043, -123.9501837107616780 ) ) ;
#174473=CARTESIAN_POINT ( 'NONE',  ( -18.40000000000000213, 64.52683809664958403, -123.8731074845243683 ) ) ;
#174530=LINE ( 'NONE', #74121, #110229 ) ;
#174546=ADVANCED_FACE ( 'NONE', ( #127261 ), #7306, .T. ) ;
#174705=CARTESIAN_POINT ( 'NONE',  ( -16.78055652883087134, 66.05322308388670649, -123.8623156469319326 ) ) ;
#174726=CARTESIAN_POINT ( 'NONE',  ( -18.40000000000000213, 64.66825945288681510, -115.6731074845243796 ) ) ;
#174861=CARTESIAN_POINT ( 'NONE',  ( -16.85312964099708566, 66.08639531794429445, -115.9202917780939686 ) ) ;
#174929=ORIENTED_EDGE ( 'NONE', *, *, #237819, .T. ) ;
#175245=ORIENTED_EDGE ( 'NONE', *, *, #163360, .T. ) ;
#175330=VERTEX_POINT ( 'NONE', #93617 ) ;
#175428=VERTEX_POINT ( 'NONE', #160033 ) ;
#175493=EDGE_LOOP ( 'NONE', ( #39026, #9100 ) ) ;
#175525=CARTESIAN_POINT ( 'NONE',  ( -12.92414019175886430, 66.58236703690573677, -118.3741590187920565 ) ) ;
#175755=DIRECTION ( 'NONE',  ( 0.000000000000000000, 1.000000000000000000, 6.982962677686266711E-15 ) ) ;
#175933=ORIENTED_EDGE ( 'NONE', *, *, #189869, .F. ) ;
#175950=ORIENTED_EDGE ( 'NONE', *, *, #52621, .F. ) ;
#176095=ORIENTED_EDGE ( 'NONE', *, *, #29325, .F. ) ;
#176113=DIRECTION ( 'NONE',  ( 0.7071067811865463515, 0.7071067811865487940, 4.937700262164540154E-15 ) ) ;
#176240=VERTEX_POINT ( 'NONE', #95565 ) ;
#176316=CARTESIAN_POINT ( 'NONE',  ( -16.85312841634287295, 66.08639382269184637, -123.6259343512318480 ) ) ;
#176420=CARTESIAN_POINT ( 'NONE',  ( -16.94052228080551714, 66.01372026691315398, -115.6327319818549455 ) ) ;
#176446=AXIS2_PLACEMENT_3D ( 'NONE', #184033, #220606, #5370 ) ;
#176463=ORIENTED_EDGE ( 'NONE', *, *, #35619, .T. ) ;
#176479=B_SPLINE_CURVE_WITH_KNOTS ( 'NONE', 3,
 ( #212714, #193154, #94024, #173633, #253098, #74523, #78311, #121347, #41795, #44348 ),
 .UNSPECIFIED., .F., .F.,
 ( 4, 3, 3, 4 ),
 ( 7.632826238681267430E-06, 4.756916949875584252E-05, 9.484459048150138379E-05, 0.0001435500935099836574 ),
 .UNSPECIFIED. ) ;
#176526=CARTESIAN_POINT ( 'NONE',  ( -18.40000000000000213, 67.17743825834568838, -127.2731074845243597 ) ) ;
#176763=AXIS2_PLACEMENT_3D ( 'NONE', #228677, #109982, #13471 ) ;
#176804=CARTESIAN_POINT ( 'NONE',  ( -15.15564720441981095, 66.58929125296495499, -118.4538990786802799 ) ) ;
#176876=DIRECTION ( 'NONE',  ( 1.000000000000000000, 0.000000000000000000, 0.000000000000000000 ) ) ;
#176963=CARTESIAN_POINT ( 'NONE',  ( 15.31784899511110076, 66.60336962369433422, -118.6160500917061000 ) ) ;
#177014=CARTESIAN_POINT ( 'NONE',  ( -16.93255653858138388, 66.00154854603491117, -123.9414641165346893 ) ) ;
#177086=CARTESIAN_POINT ( 'NONE',  ( -20.65000000000000568, 68.75000000001209344, -127.2731074845243597 ) ) ;
#177273=DIRECTION ( 'NONE',  ( -1.000000000000000000, -0.000000000000000000, -0.000000000000000000 ) ) ;
#177631=PLANE ( 'NONE',  #155604 ) ;
#177760=DIRECTION ( 'NONE',  ( 0.000000000000000000, -1.000000000000000000, -6.982962677686266711E-15 ) ) ;
#177870=VECTOR ( 'NONE', #175755, 1000.000000000000000 ) ;
#177988=LINE ( 'NONE', #78847, #107992 ) ;
#178319=EDGE_LOOP ( 'NONE', ( #208053, #89667, #27268, #5561 ) ) ;
#178336=CIRCLE ( 'NONE', #153411, 0.5000000000000004441 ) ;
#178440=EDGE_CURVE ( 'NONE', #16800, #221298, #160500, .T. ) ;
#178451=CARTESIAN_POINT ( 'NONE',  ( -17.11825945287481332, 65.95000000001201101, -115.6731074845243796 ) ) ;
#178474=CYLINDRICAL_SURFACE ( 'NONE', #114962, 1.749999999999998002 ) ;
#178492=DIRECTION ( 'NONE',  ( -0.7071067811865456854, -0.7071067811865493491, -4.937700262164544098E-15 ) ) ;
#178959=LINE ( 'NONE', #197189, #145179 ) ;
#179007=CARTESIAN_POINT ( 'NONE',  ( 20.04999999999999716, 67.25000000001205080, -123.8731074845243683 ) ) ;
#179602=CARTESIAN_POINT ( 'NONE',  ( 18.54999999999999716, 67.25000000001197975, -115.6731074845243654 ) ) ;
#179947=DIRECTION ( 'NONE',  ( -1.000000000000000000, 0.000000000000000000, 0.000000000000000000 ) ) ;
#180018=CARTESIAN_POINT ( 'NONE',  ( 22.88900146558018989, 67.29609520889925989, -127.2731074845243597 ) ) ;
#180222=ORIENTED_EDGE ( 'NONE', *, *, #242174, .F. ) ;
#180261=ORIENTED_EDGE ( 'NONE', *, *, #40436, .T. ) ;
#180449=DIRECTION ( 'NONE',  ( 0.000000000000000000, -1.000000000000000000, -6.982962677686266711E-15 ) ) ;
#180467=( LENGTH_UNIT ( ) NAMED_UNIT ( * ) SI_UNIT ( .MILLI., .METRE. ) );
#180525=DIRECTION ( 'NONE',  ( 1.186688945009010077E-16, 1.000000000000000000, 6.982962677686266711E-15 ) ) ;
#180559=ORIENTED_EDGE ( 'NONE', *, *, #10075, .T. ) ;
#180624=LINE ( 'NONE', #662, #234473 ) ;
#181057=VERTEX_POINT ( 'NONE', #250066 ) ;
#181176=ORIENTED_EDGE ( 'NONE', *, *, #155826, .F. ) ;
#181244=CYLINDRICAL_SURFACE ( 'NONE', #78156, 0.1000000000000038219 ) ;
#181444=LINE ( 'NONE', #103150, #4924 ) ;
#181485=EDGE_CURVE ( 'NONE', #79879, #186539, #257080, .T. ) ;
#181584=( BOUNDED_CURVE ( )  B_SPLINE_CURVE ( 3, ( #85026, #145021, #104589, #82459 ),
 .UNSPECIFIED., .F., .F. ) 
 B_SPLINE_CURVE_WITH_KNOTS ( ( 4, 4 ),
 ( 1.570796326794892339, 3.141592653589784678 ),
 .UNSPECIFIED. ) 
 CURVE ( )  GEOMETRIC_REPRESENTATION_ITEM ( )  RATIONAL_B_SPLINE_CURVE ( ( 1.000000000000000000, 0.8047378541243659367, 0.8047378541243659367, 1.000000000000000000 ) ) 
 REPRESENTATION_ITEM ( '' )  );
#181783=ADVANCED_FACE ( 'NONE', ( #133046 ), #169636, .F. ) ;
#181979=CARTESIAN_POINT ( 'NONE',  ( -16.86757978335471719, 66.03434962097777827, -123.9251028313568526 ) ) ;
#181999=DIRECTION ( 'NONE',  ( -0.000000000000000000, -6.982962677686266711E-15, 1.000000000000000000 ) ) ;
#182049=PRODUCT_DEFINITION_FORMATION_WITH_SPECIFIED_SOURCE ( 'ANY', '', #172353, .NOT_KNOWN. ) ;
#182087=FACE_OUTER_BOUND ( 'NONE', #102124, .T. ) ;
#182114=ORIENTED_EDGE ( 'NONE', *, *, #245029, .T. ) ;
#182212=VERTEX_POINT ( 'NONE', #17897 ) ;
#182238=LINE ( 'NONE', #192196, #212256 ) ;
#183050=ORIENTED_EDGE ( 'NONE', *, *, #37475, .T. ) ;
#183068=CARTESIAN_POINT ( 'NONE',  ( -16.93211319090181632, 66.00001321885453365, -115.6006019852513020 ) ) ;
#183109=CARTESIAN_POINT ( 'NONE',  ( -16.89155683852747103, 66.05000000001469118, -116.3004793340649741 ) ) ;
#183113=FACE_OUTER_BOUND ( 'NONE', #255224, .T. ) ;
#183192=CARTESIAN_POINT ( 'NONE',  ( 18.54999999999999716, 66.05000000001206217, -123.8731074845244251 ) ) ;
#183356=CARTESIAN_POINT ( 'NONE',  ( -16.87683809663752399, 66.05000000001207638, -123.8731074845243683 ) ) ;
#183725=VECTOR ( 'NONE', #58278, 1000.000000000000000 ) ;
#183831=ORIENTED_EDGE ( 'NONE', *, *, #152814, .T. ) ;
#183900=LINE ( 'NONE', #186474, #253935 ) ;
#184009=VERTEX_POINT ( 'NONE', #156364 ) ;
#184033=CARTESIAN_POINT ( 'NONE',  ( 23.04999999999999716, 67.17743825834557470, -112.2731074845243597 ) ) ;
#184094=CARTESIAN_POINT ( 'NONE',  ( -16.92989143108098204, 66.05000000001209060, -123.6406236097677152 ) ) ;
#184116=DIRECTION ( 'NONE',  ( 1.186688945009010077E-16, 1.000000000000000000, 6.982962677686266711E-15 ) ) ;
#184367=CARTESIAN_POINT ( 'NONE',  ( -16.87683809663752044, 66.05000000001201954, -116.4254715027206828 ) ) ;
#184412=DIRECTION ( 'NONE',  ( 0.000000000000000000, -6.982962677686266711E-15, 1.000000000000000000 ) ) ;
#184896=DIRECTION ( 'NONE',  ( 0.000000000000000000, 6.982962677686266711E-15, -1.000000000000000000 ) ) ;
#184949=ORIENTED_EDGE ( 'NONE', *, *, #67932, .F. ) ;
#185155=ORIENTED_EDGE ( 'NONE', *, *, #105400, .F. ) ;
#185382=CARTESIAN_POINT ( 'NONE',  ( -16.84421487269769813, 66.05000000001207638, -123.8536053620794348 ) ) ;
#185667=CARTESIAN_POINT ( 'NONE',  ( -16.82542659449974565, 66.06550010858458677, -115.7677430845504318 ) ) ;
#185711=FACE_OUTER_BOUND ( 'NONE', #74514, .T. ) ;
#186262=CARTESIAN_POINT ( 'NONE',  ( -18.40000000000000213, 64.52683809664949877, -112.3490535513323323 ) ) ;
#186314=DIRECTION ( 'NONE',  ( 0.7071067811865456854, 0.7071067811865493491, 4.937700262164544098E-15 ) ) ;
#186474=CARTESIAN_POINT ( 'NONE',  ( -18.40000000000000213, 64.25000000001207923, -123.8731074845243683 ) ) ;
#186539=VERTEX_POINT ( 'NONE', #41629 ) ;
#186640=CARTESIAN_POINT ( 'NONE',  ( -17.27223548802017561, 65.65460260866892384, -114.3895013053276557 ) ) ;
#186967=CARTESIAN_POINT ( 'NONE',  ( -16.97683809663752186, 66.05000000001207638, -123.1207434663278804 ) ) ;
#186978=CARTESIAN_POINT ( 'NONE',  ( -16.87998658237740912, 66.05000000001201954, -115.8867470522623080 ) ) ;
#186994=DIRECTION ( 'NONE',  ( 1.000000000000000000, 0.000000000000000000, 0.000000000000000000 ) ) ;
#187023=ORIENTED_EDGE ( 'NONE', *, *, #29729, .T. ) ;
#187155=VECTOR ( 'NONE', #8094, 1000.000000000000000 ) ;
#187197=ORIENTED_EDGE ( 'NONE', *, *, #254331, .T. ) ;
#187202=VERTEX_POINT ( 'NONE', #18713 ) ;
#187700=AXIS2_PLACEMENT_3D ( 'NONE', #117545, #195827, #17182 ) ;
#188080=ORIENTED_EDGE ( 'NONE', *, *, #135709, .F. ) ;
#188223=CARTESIAN_POINT ( 'NONE',  ( -16.88783316861822215, 66.05000000001207638, -123.7708434425445745 ) ) ;
#188228=CARTESIAN_POINT ( 'NONE',  ( -16.87036670365548474, 66.01058118071036063, -115.5435473672223168 ) ) ;
#188256=CARTESIAN_POINT ( 'NONE',  ( -16.27683809663750480, 66.65000000001209912, -127.2731074845243597 ) ) ;
#188305=CARTESIAN_POINT ( 'NONE',  ( -23.25000000000000355, 65.95000000001206786, -123.7731074845243739 ) ) ;
#188336=EDGE_CURVE ( 'NONE', #175428, #152369, #154601, .T. ) ;
#188339=ORIENTED_EDGE ( 'NONE', *, *, #56088, .T. ) ;
#188356=AXIS2_PLACEMENT_3D ( 'NONE', #108737, #164865, #86573 ) ;
#188365=DIRECTION ( 'NONE',  ( 0.000000000000000000, -1.000000000000000000, -6.789366196018718420E-15 ) ) ;
#188392=DIRECTION ( 'NONE',  ( -0.000000000000000000, -6.982962677686266711E-15, 1.000000000000000000 ) ) ;
#188571=ADVANCED_FACE ( 'NONE', ( #46169 ), #50028, .F. ) ;
#188584=VECTOR ( 'NONE', #97091, 1000.000000000000000 ) ;
#188966=DIRECTION ( 'NONE',  ( 1.186688945009010077E-16, 1.000000000000000000, 6.982962677686266711E-15 ) ) ;
#189067=DIRECTION ( 'NONE',  ( 0.000000000000000000, -1.000000000000000000, -6.982962677686266711E-15 ) ) ;
#189433=AXIS2_PLACEMENT_3D ( 'NONE', #52234, #131788, #167104 ) ;
#189434=CARTESIAN_POINT ( 'NONE',  ( -16.87683809663752399, 52.34166666667870516, -119.7731074845244592 ) ) ;
#189479=CARTESIAN_POINT ( 'NONE',  ( 14.45204356427541903, 66.54933111084451980, -121.4675609943170400 ) ) ;
#189519=CARTESIAN_POINT ( 'NONE',  ( -16.96982749440708815, 66.05000000001207638, -123.3983290757124962 ) ) ;
#189566=CARTESIAN_POINT ( 'NONE',  ( -16.90257928357874562, 66.04589317890669520, -123.8868220544106720 ) ) ;
#189668=CARTESIAN_POINT ( 'NONE',  ( 18.39999999999999503, 64.52683809664952719, -115.6731074845243796 ) ) ;
#189869=EDGE_CURVE ( 'NONE', #90904, #120700, #63149, .T. ) ;
#190066=CARTESIAN_POINT ( 'NONE',  ( 20.99999999999999645, 66.25000000001210765, -127.2731074845243597 ) ) ;
#190386=CARTESIAN_POINT ( 'NONE',  ( -18.34374000495060386, 64.52683809664961245, -127.2731074845243882 ) ) ;
#190503=CARTESIAN_POINT ( 'NONE',  ( -17.29838795458018907, 65.62845014206934025, -114.4183662019116809 ) ) ;
#190584=CARTESIAN_POINT ( 'NONE',  ( 23.24999999999999645, 70.35000000001201670, -115.6731074845243512 ) ) ;
#190599=EDGE_LOOP ( 'NONE', ( #24468, #30877, #135910, #46005 ) ) ;
#190742=CARTESIAN_POINT ( 'NONE',  ( 18.39999999999999147, 67.17743825834568838, -127.2731074845243597 ) ) ;
#190884=CARTESIAN_POINT ( 'NONE',  ( -12.25000000000000178, 66.65000000001204228, -119.7731074845243739 ) ) ;
#190930=CARTESIAN_POINT ( 'NONE',  ( 23.24999999999999645, 64.25000000001210765, -127.2731074845243882 ) ) ;
#191077=DIRECTION ( 'NONE',  ( -0.000000000000000000, -6.982962677686266711E-15, 1.000000000000000000 ) ) ;
#191189=AXIS2_PLACEMENT_3D ( 'NONE', #70160, #51825, #229217 ) ;
#191317=VECTOR ( 'NONE', #242163, 1000.000000000000000 ) ;
#191326=VERTEX_POINT ( 'NONE', #209934 ) ;
#191398=CARTESIAN_POINT ( 'NONE',  ( 18.54999999999999716, 67.25000000001205080, -123.8731074845243683 ) ) ;
#191461=LINE ( 'NONE', #151022, #50920 ) ;
#191575=VECTOR ( 'NONE', #98288, 1000.000000000000000 ) ;
#191585=DIRECTION ( 'NONE',  ( -1.073024830501117725E-15, 6.982962677686266711E-15, -1.000000000000000000 ) ) ;
#191686=CARTESIAN_POINT ( 'NONE',  ( -16.77779411503079032, 66.05389855308793301, -123.8600500669045346 ) ) ;
#191970=VERTEX_POINT ( 'NONE', #145454 ) ;
#192141=EDGE_CURVE ( 'NONE', #79398, #156548, #154491, .T. ) ;
#192196=CARTESIAN_POINT ( 'NONE',  ( -20.65000000000000568, 68.75000000001207923, -123.8731074845243540 ) ) ;
#192238=ORIENTED_EDGE ( 'NONE', *, *, #178440, .T. ) ;
#192529=CARTESIAN_POINT ( 'NONE',  ( -16.94107738177415712, 65.98576071487543970, -123.9731074845243626 ) ) ;
#192661=ORIENTED_EDGE ( 'NONE', *, *, #208436, .T. ) ;
#192678=ORIENTED_EDGE ( 'NONE', *, *, #216935, .T. ) ;
#192702=CARTESIAN_POINT ( 'NONE',  ( -16.93302609847409457, 66.00331747920884595, -123.9367189891618182 ) ) ;
#192873=ORIENTED_EDGE ( 'NONE', *, *, #118024, .T. ) ;
#192940=CARTESIAN_POINT ( 'NONE',  ( -16.77732147278574715, 66.05403306743862402, -123.8595987276485744 ) ) ;
#192943=ORIENTED_EDGE ( 'NONE', *, *, #113023, .F. ) ;
#192960=ADVANCED_FACE ( 'NONE', ( #182087 ), #140371, .F. ) ;
#193154=CARTESIAN_POINT ( 'NONE',  ( -16.88460203013675454, 66.04524099677627191, -115.6572156749861477 ) ) ;
#193310=ORIENTED_EDGE ( 'NONE', *, *, #18379, .F. ) ;
#193373=( BOUNDED_SURFACE ( )  B_SPLINE_SURFACE ( 3, 2, ( 
 ( #22061, #101544, #104126 ),
 ( #45456, #125009, #147113 ),
 ( #85833, #105391, #127567 ),
 ( #48016, #168016, #225360 ) ),
 .UNSPECIFIED., .F., .F., .F. ) 
 B_SPLINE_SURFACE_WITH_KNOTS ( ( 4, 4 ),
 ( 3, 3 ),
 ( 4.712388980384689674, 5.765869716888531116 ),
 ( 0.000000000000000000, 1.000000000000000000 ),
 .UNSPECIFIED. ) 
 GEOMETRIC_REPRESENTATION_ITEM ( )  RATIONAL_B_SPLINE_SURFACE ( (
 ( 1.000000000000000000, 0.7071067811865475727, 1.000000000000000000),
 ( 1.000000000000000000, 0.7953136715913434740, 1.000000000000000000),
 ( 1.000000000000000000, 0.8646876308615311091, 1.000000000000000000),
 ( 1.000000000000000000, 0.8984936768950603225, 1.000000000000000000) ) ) 
 REPRESENTATION_ITEM ( '' )  SURFACE ( )  );
#194721=CARTESIAN_POINT ( 'NONE',  ( -16.86445178670701850, 66.03778837089591036, -115.6323300464067643 ) ) ;
#194841=ADVANCED_FACE ( 'NONE', ( #196532 ), #75344, .F. ) ;
#194975=ORIENTED_EDGE ( 'NONE', *, *, #34309, .F. ) ;
#195001=DIRECTION ( 'NONE',  ( 0.000000000000000000, -1.000000000000000000, -6.982962677686266711E-15 ) ) ;
#195089=CARTESIAN_POINT ( 'NONE',  ( -12.60829076262179882, 66.61047060254530550, -118.7059995716306702 ) ) ;
#195244=CARTESIAN_POINT ( 'NONE',  ( -23.25000000000000355, 70.35000000001210196, -127.2731074845243313 ) ) ;
#195321=DIRECTION ( 'NONE',  ( 0.000000000000000000, 6.982962677686266711E-15, -1.000000000000000000 ) ) ;
#195493=ORIENTED_EDGE ( 'NONE', *, *, #92846, .F. ) ;
#195588=APPLICATION_CONTEXT ( 'automotive_design' ) ;
#195827=DIRECTION ( 'NONE',  ( -1.000000000000000000, 0.000000000000000000, -0.000000000000000000 ) ) ;
#196339=CARTESIAN_POINT ( 'NONE',  ( -12.24999999999999822, 66.65000000001205649, -119.6573643172504688 ) ) ;
#196486=PLANE ( 'NONE',  #106365 ) ;
#196532=FACE_OUTER_BOUND ( 'NONE', #226222, .T. ) ;
#196710=DIRECTION ( 'NONE',  ( -1.000000000000000000, 0.000000000000000000, -0.000000000000000000 ) ) ;
#197189=CARTESIAN_POINT ( 'NONE',  ( -20.65000000000000568, 70.35000000001210196, -127.2731074845243313 ) ) ;
#197244=DIRECTION ( 'NONE',  ( -1.073024830501117725E-15, -6.982962677686266711E-15, 1.000000000000000000 ) ) ;
#197620=CARTESIAN_POINT ( 'NONE',  ( -14.56336952470180357, 66.55335465531678096, -118.1123010284241985 ) ) ;
#197649=B_SPLINE_CURVE_WITH_KNOTS ( 'NONE', 3,
 ( #214615, #196339, #58092, #18982, #115516, #217171, #94669, #195089, #93386, #175525, #174266, #76378, #38560, #75146, #213325, #155964, #197620, #234174, #235460, #97195, #176804, #256243, #77658, #157250, #236740, #98477, #251162, #72567, #219749, #163645 ),
 .UNSPECIFIED., .F., .F.,
 ( 4, 2, 2, 2, 2, 2, 2, 2, 2, 2, 2, 2, 2, 2, 4 ),
 ( 0.000000000000000000, 0.0003422764154113370843, 0.0006845528308226741685, 0.001026829246234011199, 0.001369105661645348337, 0.002053658492468020229, 0.002738211323290691904, 0.003080487738702025139, 0.003422764154113358808, 0.003765040569524692043, 0.004107316984936025712, 0.004449593400347358514, 0.004791869815758693051, 0.005134146231170025852, 0.005476422646581359521 ),
 .UNSPECIFIED. ) ;
#197815=CARTESIAN_POINT ( 'NONE',  ( -16.89060415895971090, 66.04877923720985677, -123.8771872602539190 ) ) ;
#198087=VERTEX_POINT ( 'NONE', #239838 ) ;
#198333=ORIENTED_EDGE ( 'NONE', *, *, #170819, .F. ) ;
#198574=EDGE_CURVE ( 'NONE', #14308, #90904, #250108, .T. ) ;
#198612=VERTEX_POINT ( 'NONE', #255173 ) ;
#198757=CARTESIAN_POINT ( 'NONE',  ( -16.93353400591626112, 65.99538760383906322, -115.5904230143189579 ) ) ;
#198885=EDGE_LOOP ( 'NONE', ( #92359, #117041, #140537, #109730, #99870 ) ) ;
#198900=VECTOR ( 'NONE', #63412, 1000.000000000000000 ) ;
#198979=CARTESIAN_POINT ( 'NONE',  ( -17.78241384945340187, 65.14442424721026725, -126.2740698120452549 ) ) ;
#199011=CYLINDRICAL_SURFACE ( 'NONE', #237932, 0.1000000000000028644 ) ;
#199151=ADVANCED_FACE ( 'NONE', ( #28886 ), #149140, .T. ) ;
#199212=LINE ( 'NONE', #36299, #171439 ) ;
#199372=DIRECTION ( 'NONE',  ( -0.5932847527679299127, -0.8049926720990051576, -6.257843056355997642E-15 ) ) ;
#199520=CARTESIAN_POINT ( 'NONE',  ( 23.04999999999999716, 67.17743825834565996, -123.8731074845243683 ) ) ;
#199566=EDGE_CURVE ( 'NONE', #164668, #212715, #208472, .T. ) ;
#199591=VECTOR ( 'NONE', #93506, 1000.000000000000000 ) ;
#199642=EDGE_LOOP ( 'NONE', ( #193310, #226851, #109153, #35261, #175245, #107161, #180222, #34517, #120068, #219190 ) ) ;
#199735=DIRECTION ( 'NONE',  ( 1.000000000000000000, 0.000000000000000000, 0.000000000000000000 ) ) ;
#199743=EDGE_CURVE ( 'NONE', #166838, #198612, #238267, .T. ) ;
#199762=DIRECTION ( 'NONE',  ( -1.186688945009010077E-16, -1.000000000000000000, -6.789366196018717631E-15 ) ) ;
#200072=CARTESIAN_POINT ( 'NONE',  ( 17.74533788810830259, 65.18150020854118054, -113.3367301594719407 ) ) ;
#200254=CARTESIAN_POINT ( 'NONE',  ( -16.88495309932523014, 66.04537294153921323, -123.8885588107124676 ) ) ;
#200400=DIRECTION ( 'NONE',  ( -1.020425574104004196E-15, 6.982962677686266711E-15, -1.000000000000000000 ) ) ;
#200514=PLANE ( 'NONE',  #238212 ) ;
#200707=EDGE_LOOP ( 'NONE', ( #132724, #77191, #32757, #256231 ) ) ;
#200818=EDGE_LOOP ( 'NONE', ( #94836, #172450, #151184, #48619, #192873 ) ) ;
#200842=AXIS2_PLACEMENT_3D ( 'NONE', #30505, #184412, #68334 ) ;
#200948=CARTESIAN_POINT ( 'NONE',  ( 17.74533788810831325, 65.18150020854128002, -126.2094848095768072 ) ) ;
#201291=ADVANCED_FACE ( 'NONE', ( #29286 ), #108771, .T. ) ;
#201303=( LENGTH_UNIT ( ) NAMED_UNIT ( * ) SI_UNIT ( .MILLI., .METRE. ) );
#201437=CARTESIAN_POINT ( 'NONE',  ( 20.73486653747088937, 68.25000000001203659, -123.8731074845243540 ) ) ;
#201479=DIRECTION ( 'NONE',  ( -0.000000000000000000, -6.982962677686266711E-15, 1.000000000000000000 ) ) ;
#201592=DIRECTION ( 'NONE',  ( -3.035766082959430717E-14, -6.982962677686266711E-15, 1.000000000000000000 ) ) ;
#201632=EDGE_LOOP ( 'NONE', ( #205837, #133326, #53705, #232841, #29507, #54185 ) ) ;
#201653=VECTOR ( 'NONE', #1341, 1000.000000000000000 ) ;
#202630=CARTESIAN_POINT ( 'NONE',  ( -20.65000000000000568, 68.75000000001202238, -115.6731074845243512 ) ) ;
#202724=EDGE_CURVE ( 'NONE', #184009, #212706, #120488, .T. ) ;
#203560=CARTESIAN_POINT ( 'NONE',  ( -16.87683809663753465, 66.13508622147364235, -123.2473918488858544 ) ) ;
#204025=ADVANCED_FACE ( 'NONE', ( #29153, #38108, #94201 ), #159344, .T. ) ;
#204328=EDGE_LOOP ( 'NONE', ( #98303, #25847, #77703, #90475 ) ) ;
#204362=VERTEX_POINT ( 'NONE', #146169 ) ;
#204607=CARTESIAN_POINT ( 'NONE',  ( -15.75000000000000355, 66.15000000001204228, -119.7731074845243739 ) ) ;
#204761=CARTESIAN_POINT ( 'NONE',  ( 18.39999999999999503, 70.35000000001207354, -123.8731074845243398 ) ) ;
#205091=PLANE ( 'NONE',  #257426 ) ;
#205148=CARTESIAN_POINT ( 'NONE',  ( -21.64999999999999858, 65.95000000001208207, -123.8731074845243683 ) ) ;
#205208=FACE_OUTER_BOUND ( 'NONE', #137361, .T. ) ;
#205440=EDGE_LOOP ( 'NONE', ( #180261, #70026, #76654, #67797 ) ) ;
#205441=EDGE_CURVE ( 'NONE', #204362, #240802, #100923, .T. ) ;
#205506=CARTESIAN_POINT ( 'NONE',  ( -17.11825945287481332, 66.05000000001201954, -115.7731074845243597 ) ) ;
#205511=CARTESIAN_POINT ( 'NONE',  ( -17.11825945287482753, 65.95000000001206786, -123.7731074845243739 ) ) ;
#205570=CIRCLE ( 'NONE', #43294, 0.1999999999999987899 ) ;
#205576=ORIENTED_EDGE ( 'NONE', *, *, #9503, .T. ) ;
#205713=DIRECTION ( 'NONE',  ( 0.000000000000000000, 0.000000000000000000, -1.000000000000000000 ) ) ;
#205726=DIRECTION ( 'NONE',  ( 0.000000000000000000, 6.982962677686266711E-15, -1.000000000000000000 ) ) ;
#205823=EDGE_CURVE ( 'NONE', #5646, #119280, #216764, .T. ) ;
#205831=APPLICATION_CONTEXT ( 'automotive_design' ) ;
#205837=ORIENTED_EDGE ( 'NONE', *, *, #255895, .F. ) ;
#205965=CARTESIAN_POINT ( 'NONE',  ( -18.39418127959864790, 64.51609439831383952, -112.2731074845243739 ) ) ;
#206060=LINE ( 'NONE', #204761, #169527 ) ;
#206173=FACE_OUTER_BOUND ( 'NONE', #172266, .T. ) ;
#206179=ORIENTED_EDGE ( 'NONE', *, *, #142620, .F. ) ;
#206188=CARTESIAN_POINT ( 'NONE',  ( -17.22767730082837900, 65.65075578754613161, -114.3806787939587650 ) ) ;
#206218=VECTOR ( 'NONE', #248864, 1000.000000000000000 ) ;
#206283=LINE ( 'NONE', #134103, #17103 ) ;
#206511=CARTESIAN_POINT ( 'NONE',  ( -16.79270642812295833, 66.05375578307382511, -115.6841742059614688 ) ) ;
#206533=CARTESIAN_POINT ( 'NONE',  ( -33.72168855820452649, 64.52683809664949877, -112.2731074845243739 ) ) ;
#206563=CARTESIAN_POINT ( 'NONE',  ( -12.29659703204452015, 66.64411154550947458, -120.2344645877463734 ) ) ;
#206762=DIRECTION ( 'NONE',  ( 1.000000000000000000, 0.000000000000000000, 0.000000000000000000 ) ) ;
#206991=DIRECTION ( 'NONE',  ( -1.073024830501117725E-15, 6.982962677686266711E-15, -1.000000000000000000 ) ) ;
#207065=DIRECTION ( 'NONE',  ( -0.000000000000000000, -6.982962677686266711E-15, 1.000000000000000000 ) ) ;
#207069=ORIENTED_EDGE ( 'NONE', *, *, #205823, .T. ) ;
#207185=EDGE_LOOP ( 'NONE', ( #166739, #85807, #106047, #47820 ) ) ;
#207250=ORIENTED_EDGE ( 'NONE', *, *, #24452, .T. ) ;
#207374=CARTESIAN_POINT ( 'NONE',  ( -18.38639463286148867, 64.51980042617610422, -127.2731074845243882 ) ) ;
#207492=AXIS2_PLACEMENT_3D ( 'NONE', #49000, #123413, #208100 ) ;
#207504=CARTESIAN_POINT ( 'NONE',  ( -16.87331047859649757, 66.05000000001201954, -115.6731074845243796 ) ) ;
#207774=CARTESIAN_POINT ( 'NONE',  ( 12.84233041328156588, 66.58946139148318366, -121.0904194873834854 ) ) ;
#207817=CARTESIAN_POINT ( 'NONE',  ( -16.80891096016329911, 66.05000000001207638, -123.8907702917925064 ) ) ;
#207829=CARTESIAN_POINT ( 'NONE',  ( -16.84793658983450726, 66.05000000001203375, -115.7567541623343743 ) ) ;
#207981=FACE_OUTER_BOUND ( 'NONE', #248237, .T. ) ;
#208053=ORIENTED_EDGE ( 'NONE', *, *, #56463, .F. ) ;
#208088=VERTEX_POINT ( 'NONE', #159775 ) ;
#208100=DIRECTION ( 'NONE',  ( 0.000000000000000000, -6.982962677686266711E-15, 1.000000000000000000 ) ) ;
#208436=EDGE_CURVE ( 'NONE', #76307, #144523, #55696, .T. ) ;
#208472=LINE ( 'NONE', #109327, #206218 ) ;
#208671=VECTOR ( 'NONE', #177760, 1000.000000000000000 ) ;
#208976=FACE_OUTER_BOUND ( 'NONE', #164999, .T. ) ;
#209035=CARTESIAN_POINT ( 'NONE',  ( 13.22261339317535978, 66.56344716000761252, -121.3451520117640570 ) ) ;
#209071=CARTESIAN_POINT ( 'NONE',  ( -16.93710578446424009, 66.05000000001207638, -123.6043035007249671 ) ) ;
#209122=CARTESIAN_POINT ( 'NONE',  ( -15.39946565075090312, 66.61046543766534000, -120.8482981801344067 ) ) ;
#209189=ORIENTED_EDGE ( 'NONE', *, *, #6282, .F. ) ;
#209193=AXIS2_PLACEMENT_3D ( 'NONE', #55423, #234084, #54165 ) ;
#209215=CARTESIAN_POINT ( 'NONE',  ( -18.34374000495060386, 64.52683809664961245, -127.2731074845243882 ) ) ;
#209245=LINE ( 'NONE', #232687, #239990 ) ;
#209309=VECTOR ( 'NONE', #71714, 1000.000000000000000 ) ;
#209515=CARTESIAN_POINT ( 'NONE',  ( -16.94878442675512886, 66.00827089702106321, -123.9113270601622503 ) ) ;
#209934=CARTESIAN_POINT ( 'NONE',  ( 18.39999999999997371, 64.52683809664949877, -112.2731074845243739 ) ) ;
#210056=CARTESIAN_POINT ( 'NONE',  ( -17.78241384941120629, 65.14442424719840119, -113.2721451569643278 ) ) ;
#210066=CARTESIAN_POINT ( 'NONE',  ( -16.88005004766534967, 66.04989949669095495, -115.6727713725756104 ) ) ;
#210138=DIRECTION ( 'NONE',  ( 1.652117596168391700E-15, -1.000000000000000000, -6.982962677686266711E-15 ) ) ;
#210331=CARTESIAN_POINT ( 'NONE',  ( 15.70340296795548518, 66.64411154550946037, -120.2344645877463591 ) ) ;
#210366=CARTESIAN_POINT ( 'NONE',  ( -16.77180007708460963, 66.05000000001207638, -123.8874933655695543 ) ) ;
#210432=CARTESIAN_POINT ( 'NONE',  ( -15.06774609480955363, 66.58234804117103067, -121.1643200920839121 ) ) ;
#210473=DIRECTION ( 'NONE',  ( -0.000000000000000000, -6.982962677686266711E-15, 1.000000000000000000 ) ) ;
#210795=( BOUNDED_SURFACE ( )  B_SPLINE_SURFACE ( 3, 2, ( 
 ( #47419, #184367, #24043 ),
 ( #103538, #183109, #106098 ),
 ( #64438, #5713, #85241 ),
 ( #164825, #86531, #4445 ),
 ( #244341, #186978, #223489 ),
 ( #8330, #83942, #124417 ),
 ( #185667, #207829, #27908 ),
 ( #126976, #65714, #66999 ),
 ( #206511, #87820, #167411 ),
 ( #68294, #147835, #227352 ) ),
 .UNSPECIFIED., .F., .F., .F. ) 
 B_SPLINE_SURFACE_WITH_KNOTS ( ( 4, 2, 2, 2, 4 ),
 ( 3, 3 ),
 ( 0.002161241639767248670, 0.002579950749615824400, 0.002789305304540112482, 0.002893982582002256523, 0.002998659859464400564 ),
 ( 0.000000000000000000, 1.000000000000000000 ),
 .UNSPECIFIED. ) 
 GEOMETRIC_REPRESENTATION_ITEM ( )  RATIONAL_B_SPLINE_SURFACE ( (
 ( 1.000000000000000000, 0.7071067811865475727, 1.000000000000000000),
 ( 1.000000000000000000, 0.7632447400665458570, 1.000000000000000000),
 ( 1.000000000000000000, 0.8158073005108548159, 1.000000000000000000),
 ( 1.000000000000000000, 0.8906973462396701180, 1.000000000000000000),
 ( 1.000000000000000000, 0.9149408947804109626, 1.000000000000000000),
 ( 1.000000000000000000, 0.9493368785273814670, 1.000000000000000000),
 ( 1.000000000000000000, 0.9605194247155539600, 1.000000000000000000),
 ( 1.000000000000000000, 0.9803630264782379200, 1.000000000000000000),
 ( 1.000000000000000000, 0.9900844824270240707, 1.000000000000000000),
 ( 1.000000000000000000, 0.9894588281429241849, 1.000000000000000000) ) ) 
 REPRESENTATION_ITEM ( '' )  SURFACE ( )  );
#210970=EDGE_LOOP ( 'NONE', ( #223334, #82319, #84566, #158194, #97397, #98075, #80111, #54317, #98167 ) ) ;
#211202=CIRCLE ( 'NONE', #244507, 14.30833333333333890 ) ;
#211341=CARTESIAN_POINT ( 'NONE',  ( -16.87036670365549895, 66.01058118071041747, -124.0026676018264169 ) ) ;
#211480=ADVANCED_FACE ( 'NONE', ( #38763 ), #4736, .F. ) ;
#211572=CARTESIAN_POINT ( 'NONE',  ( -16.83794237512073266, 66.07364077890456144, -123.7195653258253998 ) ) ;
#211699=ORIENTED_EDGE ( 'NONE', *, *, #36486, .F. ) ;
#211709=VECTOR ( 'NONE', #46381, 1000.000000000000000 ) ;
#211710=CARTESIAN_POINT ( 'NONE',  ( -16.92778301347279424, 65.99905508317672798, -115.5945893765551915 ) ) ;
#211945=ADVANCED_FACE ( 'NONE', ( #205208 ), #210795, .F. ) ;
#212095=LINE ( 'NONE', #251183, #244776 ) ;
#212256=VECTOR ( 'NONE', #247324, 1000.000000000000000 ) ;
#212274=CIRCLE ( 'NONE', #95709, 0.9000000000000014655 ) ;
#212276=CARTESIAN_POINT ( 'NONE',  ( -16.94180778212363236, 66.00755694427991216, -123.9189239139911223 ) ) ;
#212417=CARTESIAN_POINT ( 'NONE',  ( 18.39999999999999503, 70.35000000001201670, -115.6731074845243370 ) ) ;
#212706=VERTEX_POINT ( 'NONE', #152097 ) ;
#212714=CARTESIAN_POINT ( 'NONE',  ( -16.89268316805465986, 66.04827818676982076, -115.6673550059788340 ) ) ;
#212715=VERTEX_POINT ( 'NONE', #114227 ) ;
#212891=CARTESIAN_POINT ( 'NONE',  ( 14.77516762759921498, 66.56332574816920555, -121.3462455535251792 ) ) ;
#213227=CARTESIAN_POINT ( 'NONE',  ( -17.11825945287482753, 66.05000000001207638, -123.7731074845243739 ) ) ;
#213228=CARTESIAN_POINT ( 'NONE',  ( -16.93388492042257809, 66.01145817749609535, -115.6225623613381970 ) ) ;
#213325=CARTESIAN_POINT ( 'NONE',  ( -14.22969084473441725, 66.54399267394272499, -118.0344739903776343 ) ) ;
#213483=CARTESIAN_POINT ( 'NONE',  ( 12.42718393586866021, 66.62934494888854431, -118.9972842285435064 ) ) ;
#213528=CARTESIAN_POINT ( 'NONE',  ( -16.93226657140833069, 66.00045617728764569, -123.9443943735507503 ) ) ;
#213714=DIRECTION ( 'NONE',  ( -1.073024830501117725E-15, -6.982962677686266711E-15, 1.000000000000000000 ) ) ;
#213852=MECHANICAL_DESIGN_GEOMETRIC_PRESENTATION_REPRESENTATION('',(#113894),#14146);
#213861=CARTESIAN_POINT ( 'NONE',  ( -18.40000000000000213, 70.35000000001207354, -123.8731074845243398 ) ) ;
#214082=ORIENTED_EDGE ( 'NONE', *, *, #221700, .T. ) ;
#214286=CARTESIAN_POINT ( 'NONE',  ( -18.39999999999999858, 64.52683809664961245, -127.2232782360583911 ) ) ;
#214517=CARTESIAN_POINT ( 'NONE',  ( -16.97092634996641891, 65.99911103366385134, -115.6532502508221540 ) ) ;
#214615=CARTESIAN_POINT ( 'NONE',  ( -12.25000000000000178, 66.65000000001204228, -119.7731074845243739 ) ) ;
#214714=ORIENTED_EDGE ( 'NONE', *, *, #171361, .T. ) ;
#214728=CARTESIAN_POINT ( 'NONE',  ( -18.40000000000000213, 64.25000000001202238, -115.6731074845243938 ) ) ;
#214808=CARTESIAN_POINT ( 'NONE',  ( -21.65000000000000213, 65.95000000001201101, -115.6731074845243796 ) ) ;
#214826=B_SPLINE_CURVE_WITH_KNOTS ( 'NONE', 3,
 ( #173879, #215513, #151729, #135966, #14785, #176420, #13482, #31786, #94281, #253357, #93004, #130844, #74770 ),
 .UNSPECIFIED., .F., .F.,
 ( 4, 3, 3, 3, 4 ),
 ( -3.224855718275878119E-06, 0.000000000000000000, 6.199515528664636366E-06, 4.034952380127537373E-05, 7.452715123699773787E-05 ),
 .UNSPECIFIED. ) ;
#215208=CARTESIAN_POINT ( 'NONE',  ( -16.94445028196808778, 66.00793639031432747, -123.9157773061059231 ) ) ;
#215513=CARTESIAN_POINT ( 'NONE',  ( -16.94389599337535657, 66.00880201025528038, -115.6307522863227604 ) ) ;
#215595=CIRCLE ( 'NONE', #49013, 0.9000000000000014655 ) ;
#216014=ADVANCED_FACE ( 'NONE', ( #254083 ), #78016, .T. ) ;
#216026=VECTOR ( 'NONE', #173989, 1000.000000000000000 ) ;
#216043=CARTESIAN_POINT ( 'NONE',  ( 15.07585980824113392, 66.58236703690573677, -118.3741590187920991 ) ) ;
#216295=CYLINDRICAL_SURFACE ( 'NONE', #225206, 0.1000000000000050432 ) ;
#216416=CARTESIAN_POINT ( 'NONE',  ( -16.87331047859649757, 66.05000000001201954, -115.6731074845243796 ) ) ;
#216697=CARTESIAN_POINT ( 'NONE',  ( -16.87372386987899020, 66.11939976637529526, -123.3738376126579936 ) ) ;
#216764=LINE ( 'NONE', #40741, #163439 ) ;
#216888=ORIENTED_EDGE ( 'NONE', *, *, #167658, .T. ) ;
#216935=EDGE_CURVE ( 'NONE', #7935, #37506, #239714, .T. ) ;
#217084=ORIENTED_EDGE ( 'NONE', *, *, #221105, .T. ) ;
#217146=TOROIDAL_SURFACE ( 'NONE', #75726, 14.20833333333334103, 0.1000000000000000056 ) ;
#217150=CARTESIAN_POINT ( 'NONE',  ( -16.94445028196808778, 66.00793639031432747, -123.9157773061059231 ) ) ;
#217171=CARTESIAN_POINT ( 'NONE',  ( -12.42749937872396337, 66.62931007840941788, -118.9966423578632657 ) ) ;
#217754=CARTESIAN_POINT ( 'NONE',  ( -15.55912972643741199, 67.50912972644950116, -123.9731074845243626 ) ) ;
#217771=LINE ( 'NONE', #97814, #142172 ) ;
#218602=CARTESIAN_POINT ( 'NONE',  ( 14.88075390448864788, 66.56831044948793874, -118.2438174522883116 ) ) ;
#218812=VECTOR ( 'NONE', #88611, 1000.000000000000000 ) ;
#218855=CARTESIAN_POINT ( 'NONE',  ( -15.55912972643740488, 67.50912972644943011, -115.5731074845243569 ) ) ;
#219052=CARTESIAN_POINT ( 'NONE',  ( -16.87683809663752399, 66.15000000001201386, -116.4254715027206686 ) ) ;
#219190=ORIENTED_EDGE ( 'NONE', *, *, #40306, .T. ) ;
#219357=VECTOR ( 'NONE', #152541, 1000.000000000000000 ) ;
#219404=DIRECTION ( 'NONE',  ( -1.000000000000000000, 0.000000000000000000, 0.000000000000000000 ) ) ;
#219421=ORIENTED_EDGE ( 'NONE', *, *, #22146, .T. ) ;
#219464=EDGE_LOOP ( 'NONE', ( #38851, #207250, #76751, #29976, #65606 ) ) ;
#219749=CARTESIAN_POINT ( 'NONE',  ( -15.75000000000001421, 66.65000000001205649, -119.6588398769083454 ) ) ;
#219874=CARTESIAN_POINT ( 'NONE',  ( -16.97683809663752186, 66.15000000001207070, -123.1207434663278804 ) ) ;
#219971=CARTESIAN_POINT ( 'NONE',  ( 22.88900146558018989, 67.29609520889918883, -115.6731074845243654 ) ) ;
#220451=ORIENTED_EDGE ( 'NONE', *, *, #228944, .T. ) ;
#220591=FACE_OUTER_BOUND ( 'NONE', #178319, .T. ) ;
#220606=DIRECTION ( 'NONE',  ( 0.000000000000000000, 6.982962677686266711E-15, -1.000000000000000000 ) ) ;
#221105=EDGE_CURVE ( 'NONE', #257159, #155298, #20529, .T. ) ;
#221136=CARTESIAN_POINT ( 'NONE',  ( -16.94107738177415712, 65.98576071487543970, -123.9731074845243626 ) ) ;
#221176=DIRECTION ( 'NONE',  ( 0.000000000000000000, -1.000000000000000000, -6.982962677686266711E-15 ) ) ;
#221199=CARTESIAN_POINT ( 'NONE',  ( 20.09999999999999787, 66.25000000001210765, -127.2731074845243597 ) ) ;
#221219=CARTESIAN_POINT ( 'NONE',  ( -16.88815647973234135, 66.04916738069633197, -123.8758904211983634 ) ) ;
#221298=VERTEX_POINT ( 'NONE', #34654 ) ;
#221420=ORIENTED_EDGE ( 'NONE', *, *, #230058, .T. ) ;
#221489=ORIENTED_EDGE ( 'NONE', *, *, #163986, .F. ) ;
#221700=EDGE_CURVE ( 'NONE', #16800, #33205, #25815, .T. ) ;
#221769=EDGE_LOOP ( 'NONE', ( #170140, #37791, #104042, #145427, #91820, #182114 ) ) ;
#221792=CARTESIAN_POINT ( 'NONE',  ( 20.05000000000002913, 68.75000000001197975, -115.6731074845243512 ) ) ;
#222151=CARTESIAN_POINT ( 'NONE',  ( -16.94445028196807002, 66.00793639031427062, -115.6304376629428106 ) ) ;
#222345=ORIENTED_EDGE ( 'NONE', *, *, #171384, .T. ) ;
#222348=CARTESIAN_POINT ( 'NONE',  ( -16.89268316805466341, 66.04827818676987761, -123.8788599630699281 ) ) ;
#222361=CARTESIAN_POINT ( 'NONE',  ( -18.37013991200266005, 64.50025238380011672, -127.3161304950415058 ) ) ;
#222413=ORIENTED_EDGE ( 'NONE', *, *, #5820, .T. ) ;
#222645=ORIENTED_EDGE ( 'NONE', *, *, #9503, .F. ) ;
#222700=DIRECTION ( 'NONE',  ( -1.000000000000000000, 0.000000000000000000, -0.000000000000000000 ) ) ;
#223311=ORIENTED_EDGE ( 'NONE', *, *, #4678, .F. ) ;
#223334=ORIENTED_EDGE ( 'NONE', *, *, #31567, .F. ) ;
#223466=DIRECTION ( 'NONE',  ( 0.000000000000000000, -1.000000000000000000, -6.982962677686266711E-15 ) ) ;
#223489=CARTESIAN_POINT ( 'NONE',  ( -16.92280123533721792, 66.05000000001201954, -115.8737397986094493 ) ) ;
#223494=PLANE ( 'NONE',  #146722 ) ;
#223690=ORIENTED_EDGE ( 'NONE', *, *, #31567, .T. ) ;
#224004=FACE_OUTER_BOUND ( 'NONE', #205440, .T. ) ;
#224174=LINE ( 'NONE', #204607, #88000 ) ;
#224428=EDGE_CURVE ( 'NONE', #127391, #159618, #183900, .T. ) ;
#224876=CARTESIAN_POINT ( 'NONE',  ( 20.27550659511089037, 66.78395627750316521, -115.6731074845243654 ) ) ;
#225186=DIRECTION ( 'NONE',  ( -1.020425574104004196E-15, 6.982962677686266711E-15, -1.000000000000000000 ) ) ;
#225206=AXIS2_PLACEMENT_3D ( 'NONE', #218855, #178492, #101439 ) ;
#225264=EDGE_LOOP ( 'NONE', ( #155100, #192661, #139039, #248325, #1471, #72092, #45299, #96756, #100741 ) ) ;
#225308=ADVANCED_FACE ( 'NONE', ( #56269 ), #72015, .F. ) ;
#225360=CARTESIAN_POINT ( 'NONE',  ( -16.93388492042258164, 66.01145817749616640, -123.9236526077105509 ) ) ;
#225981=( BOUNDED_SURFACE ( )  B_SPLINE_SURFACE ( 3, 2, ( 
 ( #192529, #133827, #34763 ),
 ( #70033, #8756, #229090 ),
 ( #230360, #227789, #50418 ),
 ( #209515, #10032, #90843 ) ),
 .UNSPECIFIED., .F., .F., .F. ) 
 B_SPLINE_SURFACE_WITH_KNOTS ( ( 4, 4 ),
 ( 3, 3 ),
 ( 0.0008258556059633882047, 0.0009616864997632823065 ),
 ( 0.000000000000000000, 1.000000000000000000 ),
 .UNSPECIFIED. ) 
 GEOMETRIC_REPRESENTATION_ITEM ( )  RATIONAL_B_SPLINE_SURFACE ( (
 ( 1.000000000000000000, 0.9152888060719445162, 1.000000000000000000),
 ( 1.000000000000000000, 0.9327727094138145159, 1.000000000000000000),
 ( 1.000000000000000000, 0.9369023509258376237, 1.000000000000000000),
 ( 1.000000000000000000, 0.9246339933864682337, 1.000000000000000000) ) ) 
 REPRESENTATION_ITEM ( '' )  SURFACE ( )  );
#225996=CARTESIAN_POINT ( 'NONE',  ( -16.93658211146644987, 66.00589133767080341, -115.6188124145686942 ) ) ;
#226222=EDGE_LOOP ( 'NONE', ( #101201, #226652, #90256, #96568, #106165, #29475, #1681, #26886, #126232, #18157, #3945, #44152 ) ) ;
#226293=ORIENTED_EDGE ( 'NONE', *, *, #163360, .F. ) ;
#226300=CARTESIAN_POINT ( 'NONE',  ( 20.27550659511088682, 66.78395627750323627, -127.2731074845243597 ) ) ;
#226602=CYLINDRICAL_SURFACE ( 'NONE', #61656, 0.9000000000000014655 ) ;
#226631=DIRECTION ( 'NONE',  ( -1.020425574104004196E-15, -6.982962677686266711E-15, 1.000000000000000000 ) ) ;
#226652=ORIENTED_EDGE ( 'NONE', *, *, #121235, .F. ) ;
#226851=ORIENTED_EDGE ( 'NONE', *, *, #26440, .T. ) ;
#227065=CARTESIAN_POINT ( 'NONE',  ( -16.97048326478264713, 66.05000000001207638, -123.3820006043972057 ) ) ;
#227091=DIRECTION ( 'NONE',  ( 0.5932847527679310229, 0.8049926720990042694, 6.257843056355992909E-15 ) ) ;
#227191=ORIENTED_EDGE ( 'NONE', *, *, #243430, .T. ) ;
#227258=LINE ( 'NONE', #190742, #56518 ) ;
#227265=CARTESIAN_POINT ( 'NONE',  ( -16.98495255085918032, 65.99443563401730728, -123.8884902783038768 ) ) ;
#227278=( GEOMETRIC_REPRESENTATION_CONTEXT ( 3 ) GLOBAL_UNCERTAINTY_ASSIGNED_CONTEXT ( ( #120957 ) ) GLOBAL_UNIT_ASSIGNED_CONTEXT ( ( #180467, #39698, #241720 ) ) REPRESENTATION_CONTEXT ( 'NONE', 'WORKASPACE' ) );
#227305=CARTESIAN_POINT ( 'NONE',  ( 14.87567385445976598, 66.56923500458972853, -121.2925700897739176 ) ) ;
#227352=CARTESIAN_POINT ( 'NONE',  ( -16.77180007708460963, 66.05000000001201954, -115.6587216034791936 ) ) ;
#227394=PLANE ( 'NONE',  #188356 ) ;
#227402=CARTESIAN_POINT ( 'NONE',  ( -14.56556274378147720, 66.55344247693948034, -121.4331655301784281 ) ) ;
#227503=ADVANCED_FACE ( 'NONE', ( #73894 ), #225981, .T. ) ;
#227615=AXIS2_PLACEMENT_3D ( 'NONE', #78083, #252876, #113377 ) ;
#227789=CARTESIAN_POINT ( 'NONE',  ( -16.90202395485801290, 66.03405545546117139, -123.9261212057851083 ) ) ;
#227925=FACE_OUTER_BOUND ( 'NONE', #94984, .T. ) ;
#228370=CARTESIAN_POINT ( 'NONE',  ( -16.81744102076749314, 66.05000000001207638, -123.8731074845243683 ) ) ;
#228420=LINE ( 'NONE', #190584, #25336 ) ;
#228571=CARTESIAN_POINT ( 'NONE',  ( -16.87036670365548474, 66.01058118071036063, -115.5435473672223168 ) ) ;
#228677=CARTESIAN_POINT ( 'NONE',  ( -18.40000000000000213, 70.35000000001200249, -112.2731074845243313 ) ) ;
#228944=EDGE_CURVE ( 'NONE', #98192, #9830, #209245, .T. ) ;
#228966=CARTESIAN_POINT ( 'NONE',  ( -17.01473183483381391, 66.05000000001207638, -123.7731074845243597 ) ) ;
#229090=CARTESIAN_POINT ( 'NONE',  ( -16.85718274719396703, 66.02385768539031119, -123.9597611523418976 ) ) ;
#229217=DIRECTION ( 'NONE',  ( 1.000000000000000000, 0.000000000000000000, 0.000000000000000000 ) ) ;
#229323=B_SPLINE_CURVE_WITH_KNOTS ( 'NONE', 3,
 ( #94819, #136495, #98631, #233080, #252604, #54412, #37440, #139045, #176963, #216043, #218602, #119543, #135218, #256397, #16596, #14020, #77813, #96090, #93536, #76537, #173133, #74019, #133941, #153569, #213483, #34888, #114392, #15312, #156117, #123381 ),
 .UNSPECIFIED., .F., .F.,
 ( 4, 2, 2, 2, 2, 2, 2, 2, 2, 2, 2, 2, 2, 2, 4 ),
 ( 0.000000000000000000, 0.0003422764154113352953, 0.0006845528308226705907, 0.001026829246234005778, 0.001369105661645341181, 0.002053658492468005484, 0.002738211323290670220, 0.003080487738702004756, 0.003422764154113338859, 0.003765040569524673829, 0.004107316984936008365, 0.004449593400347343769, 0.004791869815758677438, 0.005134146231170012842, 0.005476422646581347378 ),
 .UNSPECIFIED. ) ;
#229615=CARTESIAN_POINT ( 'NONE',  ( -16.77683809663752257, 66.05416425680790837, -123.8591584654201512 ) ) ;
#229622=CARTESIAN_POINT ( 'NONE',  ( -16.89268316805465986, 66.04827818676982076, -115.6673550059788340 ) ) ;
#229650=CARTESIAN_POINT ( 'NONE',  ( -16.89020380669786192, 66.05000000001207638, -123.7656963364138534 ) ) ;
#229810=EDGE_CURVE ( 'NONE', #182212, #124526, #71724, .T. ) ;
#229887=CARTESIAN_POINT ( 'NONE',  ( 13.54556439290363556, 66.54940788787835970, -121.4669191657159786 ) ) ;
#230058=EDGE_CURVE ( 'NONE', #64566, #4154, #141941, .T. ) ;
#230194=ORIENTED_EDGE ( 'NONE', *, *, #86827, .F. ) ;
#230244=AXIS2_PLACEMENT_3D ( 'NONE', #242662, #100556, #138405 ) ;
#230287=DIRECTION ( 'NONE',  ( 1.000000000000000000, 0.000000000000000000, 0.000000000000000000 ) ) ;
#230360=CARTESIAN_POINT ( 'NONE',  ( -16.92973740335413169, 66.00749618554472420, -123.9291665197261381 ) ) ;
#230410=LINE ( 'NONE', #255035, #240372 ) ;
#230668=B_SPLINE_CURVE_WITH_KNOTS ( 'NONE', 3,
 ( #10309, #166834, #162966, #127678, #45567, #44295, #105500, #85941, #165527, #125120 ),
 .UNSPECIFIED., .F., .F.,
 ( 4, 3, 3, 4 ),
 ( -2.000561356209491534E-06, 0.000000000000000000, 1.787822682428948123E-05, 4.206475347090082037E-05 ),
 .UNSPECIFIED. ) ;
#231224=CARTESIAN_POINT ( 'NONE',  ( -16.89155683852404621, 66.05000000001207638, -123.2457356349840722 ) ) ;
#231253=CARTESIAN_POINT ( 'NONE',  ( -16.81744102076749314, 66.05000000001207638, -123.8731074845243683 ) ) ;
#231275=CARTESIAN_POINT ( 'NONE',  ( -16.94107738177414291, 65.98576071487538286, -115.5731074845243711 ) ) ;
#231727=CARTESIAN_POINT ( 'NONE',  ( 18.39999999999999503, 64.25000000001207923, -123.8731074845243683 ) ) ;
#232006=ORIENTED_EDGE ( 'NONE', *, *, #95101, .F. ) ;
#232045=DIRECTION ( 'NONE',  ( -0.000000000000000000, 6.982962677686266711E-15, -1.000000000000000000 ) ) ;
#232079=CARTESIAN_POINT ( 'NONE',  ( -16.77828822508139694, 66.05377062509130326, -123.8604792331504143 ) ) ;
#232166=SHAPE_DEFINITION_REPRESENTATION ( #105440, #73451 ) ;
#232455=CIRCLE ( 'NONE', #40926, 1.500000000000001332 ) ;
#232471=CARTESIAN_POINT ( 'NONE',  ( 14.11444803880196908, 66.54256847116313622, -121.5231905466247042 ) ) ;
#232580=ADVANCED_FACE ( 'NONE', ( #89675 ), #149695, .F. ) ;
#232687=CARTESIAN_POINT ( 'NONE',  ( -21.65000000000000213, 68.75000000001207923, -123.8731074845243540 ) ) ;
#232841=ORIENTED_EDGE ( 'NONE', *, *, #83829, .T. ) ;
#232883=EDGE_CURVE ( 'NONE', #187202, #39978, #106354, .T. ) ;
#233080=CARTESIAN_POINT ( 'NONE',  ( 15.69410316191959254, 66.64325398293377134, -119.3197477631601942 ) ) ;
#233368=LINE ( 'NONE', #249068, #209309 ) ;
#233710=CARTESIAN_POINT ( 'NONE',  ( -16.79139129368504513, 66.05505583755036980, -123.8528628516985322 ) ) ;
#234019=EDGE_CURVE ( 'NONE', #156548, #241136, #75409, .T. ) ;
#234080=CARTESIAN_POINT ( 'NONE',  ( -16.91049119928363709, 66.05000000001201954, -115.6413870913335273 ) ) ;
#234084=DIRECTION ( 'NONE',  ( 0.7071067811865487940, -0.7071067811865462405, -4.216150419019403701E-15 ) ) ;
#234174=CARTESIAN_POINT ( 'NONE',  ( -14.77538296656415184, 66.56333706821293106, -118.2000707522294505 ) ) ;
#234244=CARTESIAN_POINT ( 'NONE',  ( 20.04999999999999716, 67.25000000001197975, -115.6731074845243654 ) ) ;
#234404=PLANE ( 'NONE',  #138163 ) ;
#234473=VECTOR ( 'NONE', #81479, 1000.000000000000000 ) ;
#234663=EDGE_CURVE ( 'NONE', #32814, #10416, #224174, .T. ) ;
#234794=CARTESIAN_POINT ( 'NONE',  ( -15.52965525596987817, 66.62446189796402507, -120.6532316035334986 ) ) ;
#235364=CARTESIAN_POINT ( 'NONE',  ( -17.04295772865455660, 65.97510057475052747, -115.6731074845243796 ) ) ;
#235431=ADVANCED_FACE ( 'NONE', ( #47157 ), #246659, .F. ) ;
#235460=CARTESIAN_POINT ( 'NONE',  ( -14.87770893841227249, 66.56936289831527631, -118.2548468664633958 ) ) ;
#235611=ORIENTED_EDGE ( 'NONE', *, *, #135709, .T. ) ;
#236330=ORIENTED_EDGE ( 'NONE', *, *, #240960, .T. ) ;
#236514=CARTESIAN_POINT ( 'NONE',  ( -21.64999999999999858, 65.95000000001201101, -115.6731074845243796 ) ) ;
#236740=CARTESIAN_POINT ( 'NONE',  ( -15.57281606413133268, 66.62934494888854431, -118.9972842285434638 ) ) ;
#237023=EDGE_CURVE ( 'NONE', #198612, #79398, #247781, .T. ) ;
#237080=DIRECTION ( 'NONE',  ( -0.7071067811865456854, -0.7071067811865493491, -4.937700262164544098E-15 ) ) ;
#237199=CARTESIAN_POINT ( 'NONE',  ( -16.77902162784673834, 66.05358074280420055, -123.8611162404550186 ) ) ;
#237564=( BOUNDED_SURFACE ( )  B_SPLINE_SURFACE ( 3, 2, ( 
 ( #133437, #156883, #231275 ),
 ( #35658, #36944, #211710 ),
 ( #194721, #95586, #34366 ),
 ( #33098, #52604, #172614 ) ),
 .UNSPECIFIED., .F., .F., .F. ) 
 B_SPLINE_SURFACE_WITH_KNOTS ( ( 4, 4 ),
 ( 3, 3 ),
 ( 0.0008258556059633768206, 0.0009616864997632838244 ),
 ( 0.000000000000000000, 1.000000000000000000 ),
 .UNSPECIFIED. ) 
 GEOMETRIC_REPRESENTATION_ITEM ( )  RATIONAL_B_SPLINE_SURFACE ( (
 ( 1.000000000000000000, 0.9152888060719408525, 1.000000000000000000),
 ( 1.000000000000000000, 0.9327727094137879815, 1.000000000000000000),
 ( 1.000000000000000000, 0.9369023509258773696, 1.000000000000000000),
 ( 1.000000000000000000, 0.9246339933864253791, 1.000000000000000000) ) ) 
 REPRESENTATION_ITEM ( '' )  SURFACE ( )  );
#237586=DIRECTION ( 'NONE',  ( 1.000000000000000000, -1.186688945009010077E-16, -8.286604613020808509E-31 ) ) ;
#237819=EDGE_CURVE ( 'NONE', #19871, #242236, #67622, .T. ) ;
#237932=AXIS2_PLACEMENT_3D ( 'NONE', #2072, #161173, #82871 ) ;
#237960=ORIENTED_EDGE ( 'NONE', *, *, #181485, .T. ) ;
#238212=AXIS2_PLACEMENT_3D ( 'NONE', #66137, #103952, #225186 ) ;
#238267=LINE ( 'NONE', #256493, #31287 ) ;
#238320=DIRECTION ( 'NONE',  ( -0.000000000000000000, -6.982962677686266711E-15, 1.000000000000000000 ) ) ;
#238377=DIRECTION ( 'NONE',  ( 0.000000000000000000, 6.982962677686266711E-15, -1.000000000000000000 ) ) ;
#238635=CARTESIAN_POINT ( 'NONE',  ( -16.77683809663752257, 66.05416425680785153, -115.6870565036285683 ) ) ;
#238760=FACE_OUTER_BOUND ( 'NONE', #175493, .T. ) ;
#239291=DIRECTION ( 'NONE',  ( -1.000000000000000000, 0.000000000000000000, 0.000000000000000000 ) ) ;
#239425=ORIENTED_EDGE ( 'NONE', *, *, #105400, .T. ) ;
#239526=CARTESIAN_POINT ( 'NONE',  ( -16.87331047859651179, 66.05000000001207638, -123.8731074845243683 ) ) ;
#239536=VERTEX_POINT ( 'NONE', #231253 ) ;
#239666=CARTESIAN_POINT ( 'NONE',  ( -18.40000000000000213, 64.66825945288690036, -123.8731074845243683 ) ) ;
#239714=LINE ( 'NONE', #79326, #143066 ) ;
#239751=EDGE_LOOP ( 'NONE', ( #90901, #128891, #15192, #226293 ) ) ;
#239781=EDGE_LOOP ( 'NONE', ( #219421, #21582, #42160, #50787 ) ) ;
#239838=CARTESIAN_POINT ( 'NONE',  ( 23.24999999999999645, 64.25000000001207923, -123.8731074845243683 ) ) ;
#239990=VECTOR ( 'NONE', #247077, 1000.000000000000000 ) ;
#240155=CARTESIAN_POINT ( 'NONE',  ( 20.73486653747088226, 68.75000000001203659, -123.8731074845243540 ) ) ;
#240193=CARTESIAN_POINT ( 'NONE',  ( -17.11825945287481332, 65.95000000001201101, -115.6731074845243796 ) ) ;
#240230=CARTESIAN_POINT ( 'NONE',  ( -16.89268316805465986, 66.04827818676982076, -115.6673550059788340 ) ) ;
#240277=CARTESIAN_POINT ( 'NONE',  ( -18.39999999999999858, 64.52132590001281187, -127.2484142681837227 ) ) ;
#240372=VECTOR ( 'NONE', #93451, 1000.000000000000000 ) ;
#240554=CARTESIAN_POINT ( 'NONE',  ( -15.70407651835960650, 66.64419340838190919, -120.2320049529781727 ) ) ;
#240681=ORIENTED_EDGE ( 'NONE', *, *, #66758, .F. ) ;
#240777=DIRECTION ( 'NONE',  ( 1.000000000000000000, 0.000000000000000000, 0.000000000000000000 ) ) ;
#240802=VERTEX_POINT ( 'NONE', #114199 ) ;
#240960=EDGE_CURVE ( 'NONE', #17763, #12698, #178336, .T. ) ;
#241039=ORIENTED_EDGE ( 'NONE', *, *, #243929, .T. ) ;
#241087=LINE ( 'NONE', #62436, #48647 ) ;
#241136=VERTEX_POINT ( 'NONE', #252122 ) ;
#241720=( NAMED_UNIT ( * ) SI_UNIT ( $, .STERADIAN. ) SOLID_ANGLE_UNIT ( ) );
#241971=CARTESIAN_POINT ( 'NONE',  ( -16.87036670365549895, 65.91505003675678154, -123.9731074845243626 ) ) ;
#242005=DIRECTION ( 'NONE',  ( -1.000000000000000000, 0.000000000000000000, 0.000000000000000000 ) ) ;
#242163=DIRECTION ( 'NONE',  ( -1.000000000000000000, 7.492892343619937423E-30, -1.073024830501117725E-15 ) ) ;
#242174=EDGE_CURVE ( 'NONE', #13858, #94366, #48399, .T. ) ;
#242222=ORIENTED_EDGE ( 'NONE', *, *, #56088, .F. ) ;
#242236=VERTEX_POINT ( 'NONE', #211341 ) ;
#242662=CARTESIAN_POINT ( 'NONE',  ( 13.99999999999999822, 66.15000000001204228, -119.7731074845243739 ) ) ;
#243039=CARTESIAN_POINT ( 'NONE',  ( 17.23472005113827166, 65.69211804551122214, -114.4765306244556768 ) ) ;
#243216=CARTESIAN_POINT ( 'NONE',  ( -16.87036670365549895, 66.01058118071041747, -124.0026676018264169 ) ) ;
#243430=EDGE_CURVE ( 'NONE', #10416, #240802, #128864, .T. ) ;
#243546=DIRECTION ( 'NONE',  ( 0.5932847527679299127, 0.8049926720990051576, 4.984624513800587583E-15 ) ) ;
#243562=EDGE_CURVE ( 'NONE', #98192, #186539, #217771, .T. ) ;
#243929=EDGE_CURVE ( 'NONE', #7208, #191970, #199212, .T. ) ;
#244031=CARTESIAN_POINT ( 'NONE',  ( -16.89208623190940273, 66.04842205103652475, -115.6678352813060968 ) ) ;
#244333=CARTESIAN_POINT ( 'NONE',  ( 12.25000000000000000, 66.15000000001204228, -119.7731074845243739 ) ) ;
#244341=CARTESIAN_POINT ( 'NONE',  ( -16.84981964351502270, 66.08268176591298015, -115.8927090985433352 ) ) ;
#244450=CARTESIAN_POINT ( 'NONE',  ( -18.40000000000000213, 64.52683809664949877, -112.3490535513323323 ) ) ;
#244507=AXIS2_PLACEMENT_3D ( 'NONE', #86307, #169771, #165902 ) ;
#244776=VECTOR ( 'NONE', #174289, 1000.000000000000000 ) ;
#245029=EDGE_CURVE ( 'NONE', #30013, #14308, #181584, .T. ) ;
#245631=CARTESIAN_POINT ( 'NONE',  ( -16.87401514999235275, 66.05000000001207638, -123.8031254770561844 ) ) ;
#245681=DIRECTION ( 'NONE',  ( -0.5932847527679298016, -0.8049926720990051576, -5.621233785078291429E-15 ) ) ;
#245690=CARTESIAN_POINT ( 'NONE',  ( -14.11697426661281618, 66.54258905524464751, -121.5230235107343759 ) ) ;
#246383=CARTESIAN_POINT ( 'NONE',  ( -18.38204789744325396, 64.52049896284690078, -112.2731074845243739 ) ) ;
#246405=VECTOR ( 'NONE', #71801, 1000.000000000000000 ) ;
#246630=CARTESIAN_POINT ( 'NONE',  ( -16.94225986326250677, 66.05000000001207638, -123.5763881089164755 ) ) ;
#246659=CYLINDRICAL_SURFACE ( 'NONE', #108680, 1.749999999999998002 ) ;
#246863=CARTESIAN_POINT ( 'NONE',  ( 12.47034474403011650, 66.62446189796402507, -120.6532316035334844 ) ) ;
#246899=CARTESIAN_POINT ( 'NONE',  ( -16.82055514392396489, 66.05000000001183480, -123.8463094099828368 ) ) ;
#246961=CARTESIAN_POINT ( 'NONE',  ( -14.23072895065543264, 66.54401276639934792, -121.5115763176265773 ) ) ;
#247071=ADVANCED_FACE ( 'NONE', ( #206173 ), #86190, .T. ) ;
#247077=DIRECTION ( 'NONE',  ( 1.000000000000000000, 0.000000000000000000, 0.000000000000000000 ) ) ;
#247324=DIRECTION ( 'NONE',  ( 0.000000000000000000, 1.000000000000000000, 6.982962677686266711E-15 ) ) ;
#247420=CARTESIAN_POINT ( 'NONE',  ( -20.65000000000000568, 70.35000000001210196, -127.2731074845243313 ) ) ;
#247733=LINE ( 'NONE', #152522, #48652 ) ;
#247781=CIRCLE ( 'NONE', #135332, 0.1000000000000028644 ) ;
#247870=DIRECTION ( 'NONE',  ( 1.000000000000000000, 0.000000000000000000, 0.000000000000000000 ) ) ;
#248162=CARTESIAN_POINT ( 'NONE',  ( 12.60053434924910043, 66.61046543766534000, -120.8482981801344209 ) ) ;
#248237=EDGE_LOOP ( 'NONE', ( #161204, #250330, #93771, #108707 ) ) ;
#248309=( GEOMETRIC_REPRESENTATION_CONTEXT ( 3 ) GLOBAL_UNCERTAINTY_ASSIGNED_CONTEXT ( ( #21836 ) ) GLOBAL_UNIT_ASSIGNED_CONTEXT ( ( #201303, #22700, #83881 ) ) REPRESENTATION_CONTEXT ( 'NONE', 'WORKASPACE' ) );
#248325=ORIENTED_EDGE ( 'NONE', *, *, #181485, .F. ) ;
#248566=EDGE_CURVE ( 'NONE', #19374, #94366, #93208, .T. ) ;
#248743=LINE ( 'NONE', #130056, #199591 ) ;
#248761=DIRECTION ( 'NONE',  ( -1.000000000000000000, 0.000000000000000000, 0.000000000000000000 ) ) ;
#248799=CARTESIAN_POINT ( 'NONE',  ( 18.39999999999999503, 64.25000000001202238, -115.6731074845243938 ) ) ;
#248864=DIRECTION ( 'NONE',  ( 0.000000000000000000, 6.982962677686266711E-15, -1.000000000000000000 ) ) ;
#249068=CARTESIAN_POINT ( 'NONE',  ( 20.73486653747088582, 68.75000000001205080, -127.2731074845243597 ) ) ;
#249155=LINE ( 'NONE', #213861, #246405 ) ;
#249225=DIRECTION ( 'NONE',  ( 1.000000000000000000, 0.000000000000000000, 0.000000000000000000 ) ) ;
#249391=FACE_OUTER_BOUND ( 'NONE', #239781, .T. ) ;
#249495=CARTESIAN_POINT ( 'NONE',  ( -16.87683809663752754, 66.13411015068105314, -123.2556806774542935 ) ) ;
#249513=VECTOR ( 'NONE', #219404, 1000.000000000000000 ) ;
#249609=EDGE_CURVE ( 'NONE', #105369, #55681, #86533, .T. ) ;
#249665=ADVANCED_FACE ( 'NONE', ( #183113 ), #223494, .F. ) ;
#249689=ORIENTED_EDGE ( 'NONE', *, *, #110518, .F. ) ;
#249861=LINE ( 'NONE', #132482, #249938 ) ;
#249938=VECTOR ( 'NONE', #230287, 1000.000000000000000 ) ;
#250066=CARTESIAN_POINT ( 'NONE',  ( -16.94107738177415712, 65.98576071487543970, -123.9731074845243626 ) ) ;
#250085=CARTESIAN_POINT ( 'NONE',  ( -16.93262454970419384, 65.99797953208164358, -115.5960312582870557 ) ) ;
#250108=LINE ( 'NONE', #174473, #23279 ) ;
#250115=PLANE ( 'NONE',  #38303 ) ;
#250330=ORIENTED_EDGE ( 'NONE', *, *, #40129, .T. ) ;
#250459=DIRECTION ( 'NONE',  ( 1.186688945009009831E-16, 1.000000000000000000, 6.982962677686266711E-15 ) ) ;
#250506=CARTESIAN_POINT ( 'NONE',  ( -17.78043020864321022, 65.14640788800629423, -113.3600583188041497 ) ) ;
#250757=CARTESIAN_POINT ( 'NONE',  ( -16.77308656112214535, 66.05000000001207638, -123.8729142928220455 ) ) ;
#250850=VECTOR ( 'NONE', #58904, 1000.000000000000000 ) ;
#251162=CARTESIAN_POINT ( 'NONE',  ( -15.69373346032659455, 66.64320997496614041, -119.3182809759104970 ) ) ;
#251183=CARTESIAN_POINT ( 'NONE',  ( 18.39999999999999503, 67.17743825834557470, -112.2731074845243597 ) ) ;
#251356=CARTESIAN_POINT ( 'NONE',  ( -16.94107738177414291, 65.98576071487538286, -115.5731074845243711 ) ) ;
#251643=CARTESIAN_POINT ( 'NONE',  ( 21.13736287352038445, 67.95335762362805099, -123.8731074845243540 ) ) ;
#251788=ORIENTED_EDGE ( 'NONE', *, *, #57099, .T. ) ;
#252004=CARTESIAN_POINT ( 'NONE',  ( 12.29592348164039350, 66.64419340838190919, -120.2320049529782011 ) ) ;
#252122=CARTESIAN_POINT ( 'NONE',  ( -17.11825945287482753, 66.05000000001207638, -123.7731074845243739 ) ) ;
#252196=ORIENTED_EDGE ( 'NONE', *, *, #252271, .F. ) ;
#252271=EDGE_CURVE ( 'NONE', #13858, #66849, #937, .T. ) ;
#252354=CARTESIAN_POINT ( 'NONE',  ( -16.95709691156489995, 66.05000000001200533, -115.6831650470344357 ) ) ;
#252604=CARTESIAN_POINT ( 'NONE',  ( 15.66039659514496130, 66.63925083009691264, -119.2085373439170866 ) ) ;
#252804=DIRECTION ( 'NONE',  ( 0.000000000000000000, 1.000000000000000000, 0.000000000000000000 ) ) ;
#252876=DIRECTION ( 'NONE',  ( 0.000000000000000000, -6.982962677686266711E-15, 1.000000000000000000 ) ) ;
#253098=CARTESIAN_POINT ( 'NONE',  ( -16.86733706339143524, 66.03400947037232527, -115.6199921825256638 ) ) ;
#253349=ORIENTED_EDGE ( 'NONE', *, *, #202724, .F. ) ;
#253357=CARTESIAN_POINT ( 'NONE',  ( -16.91776028072577631, 66.03659960638225357, -115.6480834698222537 ) ) ;
#253452=VECTOR ( 'NONE', #142568, 1000.000000000000000 ) ;
#253501=CIRCLE ( 'NONE', #103642, 0.09999999999999516220 ) ;
#253705=CARTESIAN_POINT ( 'NONE',  ( -23.25000000000000355, 64.25000000001202238, -115.6731074845243938 ) ) ;
#253934=CARTESIAN_POINT ( 'NONE',  ( -16.93583594267724379, 65.99137656495986448, -123.9637166452036183 ) ) ;
#253935=VECTOR ( 'NONE', #105613, 1000.000000000000000 ) ;
#254083=FACE_OUTER_BOUND ( 'NONE', #200818, .T. ) ;
#254321=CARTESIAN_POINT ( 'NONE',  ( -16.80469485234340254, 66.05784833687096125, -115.7131406405931671 ) ) ;
#254331=EDGE_CURVE ( 'NONE', #242236, #181057, #6734, .T. ) ;
#254512=CARTESIAN_POINT ( 'NONE',  ( -16.81930730667005847, 66.06300193113798969, -123.7963397539861745 ) ) ;
#254544=CARTESIAN_POINT ( 'NONE',  ( 15.74999999999999645, 66.65000000001204228, -119.7731074845243739 ) ) ;
#254564=AXIS2_PLACEMENT_3D ( 'NONE', #91603, #6918, #66898 ) ;
#254676=EDGE_LOOP ( 'NONE', ( #28733, #109310 ) ) ;
#254893=ORIENTED_EDGE ( 'NONE', *, *, #111124, .F. ) ;
#254954=CARTESIAN_POINT ( 'NONE',  ( -16.89021194854739605, 66.05000000001200533, -115.7805393529200302 ) ) ;
#255035=CARTESIAN_POINT ( 'NONE',  ( -23.25000000000000355, 70.35000000001201670, -115.6731074845243370 ) ) ;
#255171=CARTESIAN_POINT ( 'NONE',  ( -16.93970660449832621, 65.98715860837648961, -123.9708257487299079 ) ) ;
#255173=CARTESIAN_POINT ( 'NONE',  ( -21.65000000000000213, 66.05000000001207638, -123.7731074845243739 ) ) ;
#255224=EDGE_LOOP ( 'NONE', ( #171031, #173232, #128938, #78409, #147227, #223690 ) ) ;
#255270=CARTESIAN_POINT ( 'NONE',  ( -23.25000000000000355, 64.25000000001199396, -112.2731074845243739 ) ) ;
#255310=VECTOR ( 'NONE', #196710, 1000.000000000000000 ) ;
#255317=UNCERTAINTY_MEASURE_WITH_UNIT (LENGTH_MEASURE( 1.000000000000000082E-05 ), #124534, 'distance_accuracy_value', 'NONE');
#255375=CIRCLE ( 'NONE', #113956, 0.09999999999999939493 ) ;
#255562=CARTESIAN_POINT ( 'NONE',  ( -16.92925196614874750, 66.02766820360193378, -123.9063626368075859 ) ) ;
#255784=CARTESIAN_POINT ( 'NONE',  ( -16.85939591225059075, 66.09477352162421937, -123.5630392380553531 ) ) ;
#255859=EDGE_CURVE ( 'NONE', #55681, #119280, #229323, .T. ) ;
#255895=EDGE_CURVE ( 'NONE', #256630, #28814, #46386, .T. ) ;
#256229=CARTESIAN_POINT ( 'NONE',  ( -16.84419801905645997, 66.05000000001201954, -115.6925973307464091 ) ) ;
#256231=ORIENTED_EDGE ( 'NONE', *, *, #10075, .F. ) ;
#256243=CARTESIAN_POINT ( 'NONE',  ( -15.31895204843005232, 66.60346600605809897, -118.6171677053510933 ) ) ;
#256392=VERTEX_POINT ( 'NONE', #118467 ) ;
#256397=CARTESIAN_POINT ( 'NONE',  ( 13.88638282980484284, 66.54257354752311926, -118.0230656161243701 ) ) ;
#256493=CARTESIAN_POINT ( 'NONE',  ( -21.65000000000000213, 66.05000000001207638, -123.8731074845243683 ) ) ;
#256568=VERTEX_POINT ( 'NONE', #66496 ) ;
#256630=VERTEX_POINT ( 'NONE', #151175 ) ;
#257080=LINE ( 'NONE', #137178, #13014 ) ;
#257083=CARTESIAN_POINT ( 'NONE',  ( -21.65000000000000213, 68.75000000001209344, -127.2731074845243597 ) ) ;
#257123=CARTESIAN_POINT ( 'NONE',  ( -16.98495255085916611, 65.99443563401723623, -115.6577246907448853 ) ) ;
#257159=VERTEX_POINT ( 'NONE', #154732 ) ;
#257426=AXIS2_PLACEMENT_3D ( 'NONE', #91591, #72037, #151592 ) ;
#257846=ORIENTED_EDGE ( 'NONE', *, *, #36486, .T. ) ;
ENDSEC;
END-ISO-10303-21;
